ISO-10303-21;
HEADER;
FILE_DESCRIPTION (('STEP AP214'),
    '1' );
FILE_NAME ('Part 32,5_Varsayılan.step',
    '2026-10-10T17:45:43',
    ( '' ),
    ( '' ),
    'SwSTEP 2.0',
    'SolidWorks 2024',
    '' );
FILE_SCHEMA (( 'AUTOMOTIVE_DESIGN' ));
ENDSEC;

DATA;
#4=VERTEX_POINT ( 'NONE', #461 ) ;
#10=CARTESIAN_POINT ( 'NONE',  ( -13.19762691892552731, 27.23125096863189754, 3.538843351020405148 ) ) ;
#11=DIRECTION ( 'NONE',  ( -0.000000000000000000, 0.000000000000000000, 1.000000000000000000 ) ) ;
#14=FACE_OUTER_BOUND ( 'NONE', #2521, .T. ) ;
#21=ORIENTED_EDGE ( 'NONE', *, *, #6307, .T. ) ;
#22=VECTOR ( 'NONE', #3280, 1000.000000000000000 ) ;
#28=EDGE_CURVE ( 'NONE', #3551, #1184, #4957, .T. ) ;
#29=EDGE_CURVE ( 'NONE', #4703, #6200, #2516, .T. ) ;
#46=CARTESIAN_POINT ( 'NONE',  ( -174.7835321302054865, 68.75545066608756883, 12.00000000000000000 ) ) ;
#63=ORIENTED_EDGE ( 'NONE', *, *, #4361, .F. ) ;
#66=CIRCLE ( 'NONE', #4486, 12.50000000000001421 ) ;
#76=ADVANCED_FACE ( 'NONE', ( #261, #2578 ), #1123, .T. ) ;
#77=EDGE_CURVE ( 'NONE', #5794, #1266, #2476, .T. ) ;
#81=VERTEX_POINT ( 'NONE', #1223 ) ;
#83=AXIS2_PLACEMENT_3D ( 'NONE', #303, #4222, #3223 ) ;
#86=AXIS2_PLACEMENT_3D ( 'NONE', #5507, #2633, #4633 ) ;
#95=EDGE_LOOP ( 'NONE', ( #3114, #6152 ) ) ;
#96=ORIENTED_EDGE ( 'NONE', *, *, #579, .F. ) ;
#104=EDGE_CURVE ( 'NONE', #4120, #4159, #4047, .T. ) ;
#106=ORIENTED_EDGE ( 'NONE', *, *, #2540, .F. ) ;
#114=ADVANCED_FACE ( 'NONE', ( #2699 ), #6095, .F. ) ;
#129=AXIS2_PLACEMENT_3D ( 'NONE', #4697, #291, #748 ) ;
#132=DIRECTION ( 'NONE',  ( 0.000000000000000000, 1.000000000000000000, 1.247733429937938623E-16 ) ) ;
#133=CARTESIAN_POINT ( 'NONE',  ( 0.000000000000000000, 0.000000000000000000, 0.000000000000000000 ) ) ;
#135=LINE ( 'NONE', #1113, #2828 ) ;
#137=DIRECTION ( 'NONE',  ( -0.000000000000000000, 0.000000000000000000, 1.000000000000000000 ) ) ;
#148=ORIENTED_EDGE ( 'NONE', *, *, #974, .F. ) ;
#151=MANIFOLD_SOLID_BREP ( 'Cut-Extrude1', #5264 ) ;
#152=CARTESIAN_POINT ( 'NONE',  ( -6.500000000000000000, 134.5953136438507158, 12.00000000000000000 ) ) ;
#156=CYLINDRICAL_SURFACE ( 'NONE', #3481, 4.000000000000000000 ) ;
#159=PRODUCT_CONTEXT ( 'NONE', #5893, 'mechanical' ) ;
#166=AXIS2_PLACEMENT_3D ( 'NONE', #680, #1059, #2631 ) ;
#169=CIRCLE ( 'NONE', #5615, 166.8359700257217071 ) ;
#173=( NAMED_UNIT ( * ) PLANE_ANGLE_UNIT ( ) SI_UNIT ( $, .RADIAN. ) );
#185=PLANE ( 'NONE',  #3886 ) ;
#187=EDGE_CURVE ( 'NONE', #1008, #2831, #3637, .T. ) ;
#188=AXIS2_PLACEMENT_3D ( 'NONE', #6357, #4909, #956 ) ;
#192=EDGE_LOOP ( 'NONE', ( #4807, #5234, #4644, #6295 ) ) ;
#193=FACE_OUTER_BOUND ( 'NONE', #676, .T. ) ;
#203=EDGE_LOOP ( 'NONE', ( #3143, #5565 ) ) ;
#212=ORIENTED_EDGE ( 'NONE', *, *, #4955, .F. ) ;
#218=DIRECTION ( 'NONE',  ( -0.000000000000000000, -0.000000000000000000, -1.000000000000000000 ) ) ;
#227=VECTOR ( 'NONE', #4271, 1000.000000000000000 ) ;
#230=EDGE_CURVE ( 'NONE', #5659, #862, #5842, .T. ) ;
#233=ORIENTED_EDGE ( 'NONE', *, *, #2398, .F. ) ;
#238=DIRECTION ( 'NONE',  ( -1.000000000000000000, 0.000000000000000000, 0.000000000000000000 ) ) ;
#247=LINE ( 'NONE', #5691, #4727 ) ;
#256=DIRECTION ( 'NONE',  ( 0.000000000000000000, 0.000000000000000000, 1.000000000000000000 ) ) ;
#257=CARTESIAN_POINT ( 'NONE',  ( 174.7835321302054865, 68.75545066608756883, 12.00000000000000000 ) ) ;
#261=FACE_OUTER_BOUND ( 'NONE', #2435, .T. ) ;
#263=AXIS2_PLACEMENT_3D ( 'NONE', #2565, #4526, #132 ) ;
#267=ADVANCED_FACE ( 'NONE', ( #945 ), #494, .T. ) ;
#273=LINE ( 'NONE', #4092, #6243 ) ;
#276=VECTOR ( 'NONE', #3647, 1000.000000000000000 ) ;
#277=EDGE_LOOP ( 'NONE', ( #2977, #5435, #3484, #3552 ) ) ;
#281=CARTESIAN_POINT ( 'NONE',  ( -13.41482486054668044, 26.39531364385071299, 5.999999999999990230 ) ) ;
#290=CARTESIAN_POINT ( 'NONE',  ( 0.000000000000000000, 0.000000000000000000, 0.000000000000000000 ) ) ;
#291=DIRECTION ( 'NONE',  ( -0.000000000000000000, -0.000000000000000000, -1.000000000000000000 ) ) ;
#303=CARTESIAN_POINT ( 'NONE',  ( 0.000000000000000000, 120.0000000000000000, -4.000000000000000000 ) ) ;
#314=FACE_BOUND ( 'NONE', #5611, .T. ) ;
#315=EDGE_CURVE ( 'NONE', #1906, #997, #247, .T. ) ;
#316=AXIS2_PLACEMENT_3D ( 'NONE', #4448, #5394, #4967 ) ;
#318=CARTESIAN_POINT ( 'NONE',  ( -8.000000000000021316, 1.481987083124922376E-15, 12.00000000000000000 ) ) ;
#321=AXIS2_PLACEMENT_3D ( 'NONE', #133, #3087, #5016 ) ;
#326=ORIENTED_EDGE ( 'NONE', *, *, #3688, .T. ) ;
#328=VECTOR ( 'NONE', #3380, 1000.000000000000000 ) ;
#341=VERTEX_POINT ( 'NONE', #281 ) ;
#376=CARTESIAN_POINT ( 'NONE',  ( 0.000000000000000000, 0.000000000000000000, 0.000000000000000000 ) ) ;
#378=ORIENTED_EDGE ( 'NONE', *, *, #1539, .F. ) ;
#380=ORIENTED_EDGE ( 'NONE', *, *, #582, .T. ) ;
#381=DIRECTION ( 'NONE',  ( -0.000000000000000000, -0.000000000000000000, -1.000000000000000000 ) ) ;
#385=PLANE ( 'NONE',  #1235 ) ;
#386=ORIENTED_EDGE ( 'NONE', *, *, #5059, .F. ) ;
#398=CARTESIAN_POINT ( 'NONE',  ( 8.000000000000021316, 2.721075280251214820E-15, 1.999999999999986233 ) ) ;
#415=AXIS2_PLACEMENT_3D ( 'NONE', #376, #1368, #2905 ) ;
#418=DIRECTION ( 'NONE',  ( 1.852483853906148040E-16, 1.000000000000000000, 0.000000000000000000 ) ) ;
#426=CARTESIAN_POINT ( 'NONE',  ( 12.41746183822997551, 30.39531364385071655, 9.999999999999991118 ) ) ;
#428=DIRECTION ( 'NONE',  ( 0.000000000000000000, 0.000000000000000000, 1.000000000000000000 ) ) ;
#434=VERTEX_POINT ( 'NONE', #1372 ) ;
#456=CARTESIAN_POINT ( 'NONE',  ( -13.05910636442709993, 27.77388734089488054, 2.967234880352094706 ) ) ;
#461=CARTESIAN_POINT ( 'NONE',  ( -8.000000000000007105, 72.93807001241029297, 0.000000000000000000 ) ) ;
#468=DIRECTION ( 'NONE',  ( 0.000000000000000000, 0.000000000000000000, 1.000000000000000000 ) ) ;
#471=ORIENTED_EDGE ( 'NONE', *, *, #1342, .T. ) ;
#473=EDGE_CURVE ( 'NONE', #4999, #4629, #2884, .T. ) ;
#479=VECTOR ( 'NONE', #2555, 1000.000000000000000 ) ;
#484=CARTESIAN_POINT ( 'NONE',  ( 0.000000000000000000, 0.000000000000000000, 12.00000000000000000 ) ) ;
#487=LINE ( 'NONE', #5352, #1768 ) ;
#493=CARTESIAN_POINT ( 'NONE',  ( 0.000000000000000000, 120.0000000000000000, -4.000000000000000000 ) ) ;
#494=PLANE ( 'NONE',  #4742 ) ;
#495=CARTESIAN_POINT ( 'NONE',  ( -13.15471301119415237, 27.39842886758932039, 3.337628543836458572 ) ) ;
#501=CARTESIAN_POINT ( 'NONE',  ( 12.84201764556569714, 28.64001483306502038, 9.603681688880103096 ) ) ;
#506=ADVANCED_FACE ( 'NONE', ( #3791 ), #1826, .F. ) ;
#508=DIRECTION ( 'NONE',  ( -0.000000000000000000, -0.000000000000000000, -1.000000000000000000 ) ) ;
#509=ORIENTED_EDGE ( 'NONE', *, *, #679, .T. ) ;
#512=EDGE_LOOP ( 'NONE', ( #5919, #649, #3464, #3350, #1652, #1767, #4821, #6182, #378 ) ) ;
#513=EDGE_LOOP ( 'NONE', ( #2554, #1774, #6009, #4484, #4684, #1934, #3854, #3458 ) ) ;
#516=LINE ( 'NONE', #640, #2756 ) ;
#521=EDGE_CURVE ( 'NONE', #1518, #997, #1473, .T. ) ;
#525=CYLINDRICAL_SURFACE ( 'NONE', #2568, 21.00000000000000355 ) ;
#527=DIRECTION ( 'NONE',  ( -0.000000000000000000, -0.000000000000000000, -1.000000000000000000 ) ) ;
#533=CARTESIAN_POINT ( 'NONE',  ( 6.500000000000005329, 120.0000000000000000, 16.00000000000000000 ) ) ;
#536=CARTESIAN_POINT ( 'NONE',  ( 12.89883946988004659, 28.41146683342871881, 9.483046795230265502 ) ) ;
#547=DIRECTION ( 'NONE',  ( 0.000000000000000000, -1.000000000000000000, 0.000000000000000000 ) ) ;
#548=EDGE_CURVE ( 'NONE', #647, #4703, #866, .T. ) ;
#552=FACE_OUTER_BOUND ( 'NONE', #3126, .T. ) ;
#556=CARTESIAN_POINT ( 'NONE',  ( 174.7835321302054865, 68.75545066608756883, 12.00000000000000000 ) ) ;
#557=CARTESIAN_POINT ( 'NONE',  ( -6.500000000000000000, 0.000000000000000000, 12.00000000000000000 ) ) ;
#558=CARTESIAN_POINT ( 'NONE',  ( -12.41746183823000393, 30.39531364385071299, 1.999999999999990008 ) ) ;
#574=ORIENTED_EDGE ( 'NONE', *, *, #947, .F. ) ;
#579=EDGE_CURVE ( 'NONE', #5734, #4913, #1971, .T. ) ;
#582=EDGE_CURVE ( 'NONE', #2231, #3044, #4224, .T. ) ;
#596=( GEOMETRIC_REPRESENTATION_CONTEXT ( 3 ) GLOBAL_UNCERTAINTY_ASSIGNED_CONTEXT ( ( #4277 ) ) GLOBAL_UNIT_ASSIGNED_CONTEXT ( ( #4212, #3630, #5802 ) ) REPRESENTATION_CONTEXT ( 'NONE', 'WORKASPACE' ) );
#607=EDGE_CURVE ( 'NONE', #1184, #5794, #4422, .T. ) ;
#611=DIRECTION ( 'NONE',  ( 0.000000000000000000, -1.000000000000000000, 0.000000000000000000 ) ) ;
#612=B_SPLINE_CURVE_WITH_KNOTS ( 'NONE', 3,
 ( #4261, #1894, #1864, #2817, #5344, #3852, #5730, #3825, #5798, #5379, #3329, #927, #6245, #5309, #1345, #5824, #1827, #5862 ),
 .UNSPECIFIED., .F., .F.,
 ( 4, 2, 2, 2, 2, 2, 2, 2, 4 ),
 ( 0.000000000000000000, 0.0007936035350328095447, 0.001587207070065619089, 0.002380810605098428526, 0.003174414140131238179, 0.003968017675164047832, 0.004761621210196857051, 0.005555224745229667138, 0.006348828280262476358 ),
 .UNSPECIFIED. ) ;
#618=EDGE_LOOP ( 'NONE', ( #4862, #1550, #6154, #2406 ) ) ;
#640=CARTESIAN_POINT ( 'NONE',  ( -17.05141243254543681, 0.000000000000000000, 12.00000000000000000 ) ) ;
#643=VERTEX_POINT ( 'NONE', #5521 ) ;
#646=CARTESIAN_POINT ( 'NONE',  ( 174.7835321302054865, 68.75545066608756883, 12.00000000000000000 ) ) ;
#647=VERTEX_POINT ( 'NONE', #152 ) ;
#649=ORIENTED_EDGE ( 'NONE', *, *, #1493, .F. ) ;
#651=CARTESIAN_POINT ( 'NONE',  ( 0.000000000000000000, 0.000000000000000000, 16.00000000000000000 ) ) ;
#655=DIRECTION ( 'NONE',  ( -0.000000000000000000, -0.000000000000000000, -1.000000000000000000 ) ) ;
#660=EDGE_CURVE ( 'NONE', #4451, #1805, #3400, .T. ) ;
#664=EDGE_CURVE ( 'NONE', #1786, #1760, #2432, .T. ) ;
#666=CARTESIAN_POINT ( 'NONE',  ( 13.00793927997764321, 27.97619002235532903, 2.803925835876298844 ) ) ;
#675=DIRECTION ( 'NONE',  ( 1.000000000000000000, 3.576835832488757469E-15, 0.000000000000000000 ) ) ;
#676=EDGE_LOOP ( 'NONE', ( #5922, #4982, #4164, #5464 ) ) ;
#679=EDGE_CURVE ( 'NONE', #3152, #647, #1047, .T. ) ;
#680=CARTESIAN_POINT ( 'NONE',  ( 0.000000000000000000, 120.0000000000000000, 16.00000000000000000 ) ) ;
#695=ORIENTED_EDGE ( 'NONE', *, *, #3688, .F. ) ;
#699=EDGE_CURVE ( 'NONE', #862, #6200, #5684, .T. ) ;
#700=EDGE_CURVE ( 'NONE', #2130, #4703, #273, .T. ) ;
#701=CARTESIAN_POINT ( 'NONE',  ( 6.500000000000000000, 130.6770782520313219, 0.000000000000000000 ) ) ;
#724=DIRECTION ( 'NONE',  ( 0.000000000000000000, -1.000000000000000000, -1.247733429937938623E-16 ) ) ;
#737=CARTESIAN_POINT ( 'NONE',  ( -8.000000000000007105, 72.93807001241029297, 12.00000000000000000 ) ) ;
#748=DIRECTION ( 'NONE',  ( -1.000000000000000000, 0.000000000000000000, 0.000000000000000000 ) ) ;
#757=CARTESIAN_POINT ( 'NONE',  ( -17.05141243254543681, -24.25762350764758679, 0.000000000000000000 ) ) ;
#786=EDGE_CURVE ( 'NONE', #3016, #2696, #2527, .T. ) ;
#800=ORIENTED_EDGE ( 'NONE', *, *, #6223, .T. ) ;
#806=CARTESIAN_POINT ( 'NONE',  ( -8.000000000000007105, 72.93807001241029297, 12.00000000000000000 ) ) ;
#808=DIRECTION ( 'NONE',  ( 0.000000000000000000, -0.000000000000000000, -1.000000000000000000 ) ) ;
#809=FACE_OUTER_BOUND ( 'NONE', #513, .T. ) ;
#821=ORIENTED_EDGE ( 'NONE', *, *, #4137, .F. ) ;
#823=VERTEX_POINT ( 'NONE', #4229 ) ;
#826=DIRECTION ( 'NONE',  ( 1.000000000000000000, 0.000000000000000000, 0.000000000000000000 ) ) ;
#828=DIRECTION ( 'NONE',  ( -1.000000000000000000, 0.000000000000000000, 0.000000000000000000 ) ) ;
#831=EDGE_LOOP ( 'NONE', ( #233, #3348, #2987, #821 ) ) ;
#843=CARTESIAN_POINT ( 'NONE',  ( 19.25293315802950644, 8.385974291186926166, 0.000000000000000000 ) ) ;
#848=EDGE_LOOP ( 'NONE', ( #6233, #2139, #3706, #4614 ) ) ;
#856=CARTESIAN_POINT ( 'NONE',  ( -21.00000000000000355, 0.000000000000000000, 12.00000000000000000 ) ) ;
#862=VERTEX_POINT ( 'NONE', #701 ) ;
#866=LINE ( 'NONE', #4785, #2269 ) ;
#870=FACE_OUTER_BOUND ( 'NONE', #2801, .T. ) ;
#876=CARTESIAN_POINT ( 'NONE',  ( 6.500000000000000000, 0.000000000000000000, 12.00000000000000000 ) ) ;
#881=PLANE ( 'NONE',  #4790 ) ;
#888=DIRECTION ( 'NONE',  ( 1.000000000000000000, 0.000000000000000000, 0.000000000000000000 ) ) ;
#890=ORIENTED_EDGE ( 'NONE', *, *, #2776, .T. ) ;
#896=CIRCLE ( 'NONE', #1523, 21.00000000000000355 ) ;
#902=DIRECTION ( 'NONE',  ( 0.000000000000000000, 1.000000000000000000, 1.239088197126290570E-16 ) ) ;
#908=CIRCLE ( 'NONE', #5628, 21.00000000000000355 ) ;
#912=CARTESIAN_POINT ( 'NONE',  ( 8.000000000000007105, 72.93807001241029297, 12.00000000000000000 ) ) ;
#924=AXIS2_PLACEMENT_3D ( 'NONE', #2743, #4649, #5658 ) ;
#925=CIRCLE ( 'NONE', #4616, 21.00000000000000355 ) ;
#927=CARTESIAN_POINT ( 'NONE',  ( -13.27340567884428957, 26.93747317953756593, 8.027960515371221462 ) ) ;
#934=DIRECTION ( 'NONE',  ( 0.000000000000000000, -1.000000000000000000, 0.000000000000000000 ) ) ;
#940=ADVANCED_FACE ( 'NONE', ( #3908 ), #2902, .F. ) ;
#945=FACE_OUTER_BOUND ( 'NONE', #2573, .T. ) ;
#946=EDGE_CURVE ( 'NONE', #3551, #4017, #5790, .T. ) ;
#947=EDGE_CURVE ( 'NONE', #3745, #4120, #66, .T. ) ;
#948=DIRECTION ( 'NONE',  ( 0.000000000000000000, 0.000000000000000000, 1.000000000000000000 ) ) ;
#956=DIRECTION ( 'NONE',  ( 1.000000000000000000, 0.000000000000000000, 0.000000000000000000 ) ) ;
#966=DIRECTION ( 'NONE',  ( 0.000000000000000000, -0.000000000000000000, -1.000000000000000000 ) ) ;
#973=CARTESIAN_POINT ( 'NONE',  ( -8.000000000000007105, 72.93807001241029297, 9.999999999999996447 ) ) ;
#974=EDGE_CURVE ( 'NONE', #3152, #2130, #3352, .T. ) ;
#975=CARTESIAN_POINT ( 'NONE',  ( -13.30660938351090117, 26.80958678890347358, 4.207676383415306809 ) ) ;
#987=ORIENTED_EDGE ( 'NONE', *, *, #2859, .F. ) ;
#990=VERTEX_POINT ( 'NONE', #5758 ) ;
#997=VERTEX_POINT ( 'NONE', #3816 ) ;
#1002=ORIENTED_EDGE ( 'NONE', *, *, #28, .T. ) ;
#1008=VERTEX_POINT ( 'NONE', #1821 ) ;
#1010=CARTESIAN_POINT ( 'NONE',  ( 13.41482486054666445, 26.39531364385071655, 6.264720534548224862 ) ) ;
#1011=CARTESIAN_POINT ( 'NONE',  ( 0.000000000000000000, 0.000000000000000000, 16.00000000000000000 ) ) ;
#1022=DIRECTION ( 'NONE',  ( 1.000000000000000000, 0.000000000000000000, 0.000000000000000000 ) ) ;
#1026=VECTOR ( 'NONE', #508, 1000.000000000000000 ) ;
#1028=DIRECTION ( 'NONE',  ( 1.000000000000000000, 0.000000000000000000, 0.000000000000000000 ) ) ;
#1029=FACE_OUTER_BOUND ( 'NONE', #5572, .T. ) ;
#1039=ORIENTED_EDGE ( 'NONE', *, *, #2197, .F. ) ;
#1047=LINE ( 'NONE', #1620, #6135 ) ;
#1051=ORIENTED_EDGE ( 'NONE', *, *, #2508, .F. ) ;
#1055=DIRECTION ( 'NONE',  ( 1.000000000000000000, 1.852483853906148040E-16, -0.000000000000000000 ) ) ;
#1057=DIRECTION ( 'NONE',  ( 1.000000000000000000, 0.000000000000000000, -0.000000000000000000 ) ) ;
#1059=DIRECTION ( 'NONE',  ( 0.000000000000000000, 0.000000000000000000, 1.000000000000000000 ) ) ;
#1069=CARTESIAN_POINT ( 'NONE',  ( 7.947562104483774093, 68.75545066608756883, 0.000000000000000000 ) ) ;
#1075=DIRECTION ( 'NONE',  ( -0.000000000000000000, -0.000000000000000000, -1.000000000000000000 ) ) ;
#1082=EDGE_LOOP ( 'NONE', ( #1739, #987 ) ) ;
#1095=EDGE_LOOP ( 'NONE', ( #6109, #1616, #3312, #3605, #890, #5404, #5243 ) ) ;
#1099=DIRECTION ( 'NONE',  ( 1.000000000000000000, 0.000000000000000000, 0.000000000000000000 ) ) ;
#1102=FACE_OUTER_BOUND ( 'NONE', #5593, .T. ) ;
#1104=ORIENTED_EDGE ( 'NONE', *, *, #664, .F. ) ;
#1106=DIRECTION ( 'NONE',  ( 1.000000000000000000, 0.000000000000000000, 0.000000000000000000 ) ) ;
#1108=VECTOR ( 'NONE', #418, 1000.000000000000000 ) ;
#1113=CARTESIAN_POINT ( 'NONE',  ( -16.00000000000000000, 0.000000000000000000, 12.00000000000000000 ) ) ;
#1114=VECTOR ( 'NONE', #218, 1000.000000000000000 ) ;
#1123=CYLINDRICAL_SURFACE ( 'NONE', #1649, 21.00000000000000355 ) ;
#1127=ADVANCED_FACE ( 'NONE', ( #4972, #2492 ), #2604, .T. ) ;
#1129=CARTESIAN_POINT ( 'NONE',  ( -6.500000000000001776, 120.0000000000000000, 12.00000000000000000 ) ) ;
#1141=ORIENTED_EDGE ( 'NONE', *, *, #5072, .T. ) ;
#1143=LINE ( 'NONE', #5114, #1391 ) ;
#1157=DIRECTION ( 'NONE',  ( -0.000000000000000000, -0.000000000000000000, -1.000000000000000000 ) ) ;
#1175=ORIENTED_EDGE ( 'NONE', *, *, #2540, .T. ) ;
#1182=DIRECTION ( 'NONE',  ( -1.000000000000000000, -1.852483853906148286E-16, 0.000000000000000000 ) ) ;
#1184=VERTEX_POINT ( 'NONE', #2279 ) ;
#1194=EDGE_CURVE ( 'NONE', #2036, #1301, #4241, .T. ) ;
#1196=CARTESIAN_POINT ( 'NONE',  ( -19.25293315802950644, 8.385974291186926166, 12.00000000000000000 ) ) ;
#1199=LINE ( 'NONE', #3649, #2462 ) ;
#1204=CIRCLE ( 'NONE', #1404, 12.50000000000001421 ) ;
#1207=ORIENTED_EDGE ( 'NONE', *, *, #1789, .F. ) ;
#1212=UNCERTAINTY_MEASURE_WITH_UNIT (LENGTH_MEASURE( 1.000000000000000082E-05 ), #3670, 'distance_accuracy_value', 'NONE');
#1218=EDGE_LOOP ( 'NONE', ( #2428, #21, #96, #6326 ) ) ;
#1223=CARTESIAN_POINT ( 'NONE',  ( 21.00000000000000355, 2.571758278209442056E-15, -4.000000000000000000 ) ) ;
#1230=AXIS2_PLACEMENT_3D ( 'NONE', #5873, #2993, #2891 ) ;
#1235=AXIS2_PLACEMENT_3D ( 'NONE', #4263, #1766, #6246 ) ;
#1236=CYLINDRICAL_SURFACE ( 'NONE', #924, 12.50000000000000355 ) ;
#1247=EDGE_CURVE ( 'NONE', #1008, #2696, #3309, .T. ) ;
#1248=VECTOR ( 'NONE', #934, 1000.000000000000000 ) ;
#1250=DIRECTION ( 'NONE',  ( -0.000000000000000000, 0.000000000000000000, 1.000000000000000000 ) ) ;
#1251=CARTESIAN_POINT ( 'NONE',  ( -8.000000000000021316, 1.481987083124922376E-15, 12.00000000000000000 ) ) ;
#1255=ORIENTED_EDGE ( 'NONE', *, *, #1640, .T. ) ;
#1257=ORIENTED_EDGE ( 'NONE', *, *, #2398, .T. ) ;
#1265=ORIENTED_EDGE ( 'NONE', *, *, #77, .T. ) ;
#1266=VERTEX_POINT ( 'NONE', #5159 ) ;
#1270=CARTESIAN_POINT ( 'NONE',  ( 0.000000000000000000, 120.0000000000000000, 0.000000000000000000 ) ) ;
#1278=VERTEX_POINT ( 'NONE', #843 ) ;
#1281=CARTESIAN_POINT ( 'NONE',  ( -12.50000000000001421, 120.0000000000000000, -4.000000000000000000 ) ) ;
#1284=EDGE_LOOP ( 'NONE', ( #2202, #3694 ) ) ;
#1293=VERTEX_POINT ( 'NONE', #1281 ) ;
#1296=AXIS2_PLACEMENT_3D ( 'NONE', #556, #808, #2719 ) ;
#1301=VERTEX_POINT ( 'NONE', #4794 ) ;
#1302=AXIS2_PLACEMENT_3D ( 'NONE', #3078, #2592, #5834 ) ;
#1308=EDGE_LOOP ( 'NONE', ( #1848, #5996 ) ) ;
#1309=AXIS2_PLACEMENT_3D ( 'NONE', #5239, #3391, #2263 ) ;
#1318=ORIENTED_EDGE ( 'NONE', *, *, #1367, .T. ) ;
#1322=ADVANCED_FACE ( 'NONE', ( #3214, #2720 ), #5638, .T. ) ;
#1331=ADVANCED_FACE ( 'NONE', ( #809 ), #3702, .T. ) ;
#1332=CIRCLE ( 'NONE', #2148, 166.8359700257217071 ) ;
#1336=DIRECTION ( 'NONE',  ( -0.000000000000000000, -0.000000000000000000, -1.000000000000000000 ) ) ;
#1341=PRODUCT_DEFINITION ( 'UNKNOWN', '', #3028, #4696 ) ;
#1342=EDGE_CURVE ( 'NONE', #3225, #2036, #3246, .T. ) ;
#1345=CARTESIAN_POINT ( 'NONE',  ( -13.38016919228157420, 26.52751760200100861, 7.054451311141072267 ) ) ;
#1352=CARTESIAN_POINT ( 'NONE',  ( 6.500000000000000000, 134.5953136438507158, 0.000000000000000000 ) ) ;
#1357=ADVANCED_FACE ( 'NONE', ( #552 ), #5446, .T. ) ;
#1367=EDGE_CURVE ( 'NONE', #5659, #3460, #487, .T. ) ;
#1368=DIRECTION ( 'NONE',  ( -0.000000000000000000, 0.000000000000000000, 1.000000000000000000 ) ) ;
#1372=CARTESIAN_POINT ( 'NONE',  ( -21.00000000000000355, 0.000000000000000000, -4.000000000000000000 ) ) ;
#1375=EDGE_LOOP ( 'NONE', ( #1991, #4978 ) ) ;
#1383=CARTESIAN_POINT ( 'NONE',  ( 6.500000000000000000, 130.6770782520313219, 12.00000000000000000 ) ) ;
#1390=DIRECTION ( 'NONE',  ( 0.000000000000000000, 0.000000000000000000, 1.000000000000000000 ) ) ;
#1391=VECTOR ( 'NONE', #4591, 1000.000000000000000 ) ;
#1404=AXIS2_PLACEMENT_3D ( 'NONE', #1696, #137, #6120 ) ;
#1407=ORIENTED_EDGE ( 'NONE', *, *, #699, .T. ) ;
#1430=DIRECTION ( 'NONE',  ( 0.000000000000000000, 0.000000000000000000, 1.000000000000000000 ) ) ;
#1433=VERTEX_POINT ( 'NONE', #2956 ) ;
#1448=CARTESIAN_POINT ( 'NONE',  ( 17.05141243254543681, -12.25762350764760455, 0.000000000000000000 ) ) ;
#1449=EDGE_CURVE ( 'NONE', #3460, #6200, #1143, .T. ) ;
#1458=CARTESIAN_POINT ( 'NONE',  ( -12.54137761259614159, 29.87368101119750818, 2.025772336917470717 ) ) ;
#1473=LINE ( 'NONE', #5823, #3715 ) ;
#1481=CARTESIAN_POINT ( 'NONE',  ( 8.000000000000001776, 100.3953136438507272, 5.999999999999999112 ) ) ;
#1482=EDGE_LOOP ( 'NONE', ( #2941, #5890, #5376, #3270 ) ) ;
#1483=CARTESIAN_POINT ( 'NONE',  ( -6.500000000000000000, 134.5953136438507158, 0.000000000000000000 ) ) ;
#1486=EDGE_CURVE ( 'NONE', #3225, #6319, #5007, .T. ) ;
#1491=CARTESIAN_POINT ( 'NONE',  ( 13.38016919228157420, 26.52751760200101216, 7.054451311141071379 ) ) ;
#1492=CARTESIAN_POINT ( 'NONE',  ( 174.7835321302054865, 68.75545066608756883, 12.00000000000000000 ) ) ;
#1493=EDGE_CURVE ( 'NONE', #4451, #5912, #169, .T. ) ;
#1500=CARTESIAN_POINT ( 'NONE',  ( 13.05910636442709993, 27.77388734089489120, 2.967234880352092929 ) ) ;
#1512=CIRCLE ( 'NONE', #1302, 166.8359700257217071 ) ;
#1515=CARTESIAN_POINT ( 'NONE',  ( 0.000000000000000000, 120.0000000000000000, 16.00000000000000000 ) ) ;
#1517=CARTESIAN_POINT ( 'NONE',  ( 8.000000000000021316, 1.481987083124922376E-15, 0.000000000000000000 ) ) ;
#1518=VERTEX_POINT ( 'NONE', #4102 ) ;
#1519=CARTESIAN_POINT ( 'NONE',  ( 174.7835321302054865, 68.75545066608756883, 1.999999999999994893 ) ) ;
#1520=CARTESIAN_POINT ( 'NONE',  ( 12.54049055679404212, 29.87738611749457718, 9.974675204776747961 ) ) ;
#1523=AXIS2_PLACEMENT_3D ( 'NONE', #6284, #6188, #2757 ) ;
#1529=ORIENTED_EDGE ( 'NONE', *, *, #5548, .F. ) ;
#1533=DIRECTION ( 'NONE',  ( 1.000000000000000000, 0.000000000000000000, 0.000000000000000000 ) ) ;
#1539=EDGE_CURVE ( 'NONE', #3044, #3551, #4683, .T. ) ;
#1545=VECTOR ( 'NONE', #1866, 1000.000000000000000 ) ;
#1547=VECTOR ( 'NONE', #3052, 1000.000000000000000 ) ;
#1550=ORIENTED_EDGE ( 'NONE', *, *, #664, .T. ) ;
#1553=CARTESIAN_POINT ( 'NONE',  ( 13.15428815592193956, 27.40009807703880540, 8.663997969339835237 ) ) ;
#1555=DIRECTION ( 'NONE',  ( 1.852483853906148040E-16, 1.000000000000000000, 1.239088197126290570E-16 ) ) ;
#1566=DIRECTION ( 'NONE',  ( 0.000000000000000000, -0.000000000000000000, -1.000000000000000000 ) ) ;
#1568=DIRECTION ( 'NONE',  ( -0.000000000000000000, -0.000000000000000000, -1.000000000000000000 ) ) ;
#1584=EDGE_CURVE ( 'NONE', #5526, #4, #5827, .T. ) ;
#1600=EDGE_CURVE ( 'NONE', #4629, #4999, #6335, .T. ) ;
#1602=DIRECTION ( 'NONE',  ( -0.000000000000000000, -0.000000000000000000, -1.000000000000000000 ) ) ;
#1616=ORIENTED_EDGE ( 'NONE', *, *, #4955, .T. ) ;
#1618=ORIENTED_EDGE ( 'NONE', *, *, #1449, .F. ) ;
#1619=LINE ( 'NONE', #856, #4240 ) ;
#1620=CARTESIAN_POINT ( 'NONE',  ( -6.500000000000000000, 0.000000000000000000, 12.00000000000000000 ) ) ;
#1621=LINE ( 'NONE', #5561, #1114 ) ;
#1624=CARTESIAN_POINT ( 'NONE',  ( 18.00000000000001421, 30.39531364385072010, 5.999999999999990230 ) ) ;
#1626=EDGE_CURVE ( 'NONE', #434, #81, #6028, .T. ) ;
#1634=ORIENTED_EDGE ( 'NONE', *, *, #5625, .T. ) ;
#1638=ADVANCED_FACE ( 'NONE', ( #5617 ), #2076, .F. ) ;
#1640=EDGE_CURVE ( 'NONE', #1805, #5526, #5135, .T. ) ;
#1642=DIRECTION ( 'NONE',  ( -0.000000000000000000, -0.000000000000000000, -1.000000000000000000 ) ) ;
#1649=AXIS2_PLACEMENT_3D ( 'NONE', #3095, #3187, #6033 ) ;
#1652=ORIENTED_EDGE ( 'NONE', *, *, #5237, .F. ) ;
#1653=DIRECTION ( 'NONE',  ( 0.000000000000000000, -1.000000000000000000, 0.000000000000000000 ) ) ;
#1655=VECTOR ( 'NONE', #1157, 1000.000000000000000 ) ;
#1658=CARTESIAN_POINT ( 'NONE',  ( 8.000000000000007105, 72.93807001241029297, 0.000000000000000000 ) ) ;
#1663=ORIENTED_EDGE ( 'NONE', *, *, #660, .T. ) ;
#1677=ORIENTED_EDGE ( 'NONE', *, *, #5795, .T. ) ;
#1682=DIRECTION ( 'NONE',  ( 0.000000000000000000, 1.000000000000000000, -0.000000000000000000 ) ) ;
#1692=CARTESIAN_POINT ( 'NONE',  ( -6.500000000000005329, 120.0000000000000000, 16.00000000000000000 ) ) ;
#1696=CARTESIAN_POINT ( 'NONE',  ( 0.000000000000000000, 120.0000000000000000, 0.000000000000000000 ) ) ;
#1704=CARTESIAN_POINT ( 'NONE',  ( 0.000000000000000000, 120.0000000000000000, 12.00000000000000000 ) ) ;
#1708=ORIENTED_EDGE ( 'NONE', *, *, #4886, .T. ) ;
#1710=CIRCLE ( 'NONE', #4388, 4.000000000000003553 ) ;
#1726=ORIENTED_EDGE ( 'NONE', *, *, #1194, .T. ) ;
#1727=LINE ( 'NONE', #4691, #1545 ) ;
#1739=ORIENTED_EDGE ( 'NONE', *, *, #2123, .F. ) ;
#1760=VERTEX_POINT ( 'NONE', #4056 ) ;
#1761=STYLED_ITEM('',(#6391),#151);
#1763=DIRECTION ( 'NONE',  ( 1.000000000000000000, 0.000000000000000000, 0.000000000000000000 ) ) ;
#1766=DIRECTION ( 'NONE',  ( 0.000000000000000000, 1.000000000000000000, 0.000000000000000000 ) ) ;
#1767=ORIENTED_EDGE ( 'NONE', *, *, #77, .F. ) ;
#1768=VECTOR ( 'NONE', #1930, 1000.000000000000000 ) ;
#1774=ORIENTED_EDGE ( 'NONE', *, *, #6177, .T. ) ;
#1785=DIRECTION ( 'NONE',  ( -0.000000000000000000, 0.000000000000000000, 1.000000000000000000 ) ) ;
#1786=VERTEX_POINT ( 'NONE', #5004 ) ;
#1789=EDGE_CURVE ( 'NONE', #2013, #434, #1619, .T. ) ;
#1792=DIRECTION ( 'NONE',  ( 0.000000000000000000, 0.000000000000000000, 1.000000000000000000 ) ) ;
#1804=DIRECTION ( 'NONE',  ( 0.000000000000000000, 0.000000000000000000, 1.000000000000000000 ) ) ;
#1805=VERTEX_POINT ( 'NONE', #3195 ) ;
#1809=ORIENTED_EDGE ( 'NONE', *, *, #2656, .T. ) ;
#1812=CIRCLE ( 'NONE', #3451, 12.50000000000001421 ) ;
#1814=CARTESIAN_POINT ( 'NONE',  ( -17.05141243254543681, -24.25762350764758679, 12.00000000000000000 ) ) ;
#1819=DIRECTION ( 'NONE',  ( -0.000000000000000000, -0.000000000000000000, -1.000000000000000000 ) ) ;
#1820=CIRCLE ( 'NONE', #5111, 166.8359700257217071 ) ;
#1821=CARTESIAN_POINT ( 'NONE',  ( 8.000000000000007105, 72.93807001241029297, 1.999999999999996669 ) ) ;
#1823=PLANE ( 'NONE',  #415 ) ;
#1826=PLANE ( 'NONE',  #4950 ) ;
#1827=CARTESIAN_POINT ( 'NONE',  ( -13.41482486054669820, 26.39531364385071299, 6.264720534548226638 ) ) ;
#1829=ADVANCED_FACE ( 'NONE', ( #14 ), #2930, .F. ) ;
#1848=ORIENTED_EDGE ( 'NONE', *, *, #3527, .T. ) ;
#1855=DIRECTION ( 'NONE',  ( 1.000000000000000000, 0.000000000000000000, 0.000000000000000000 ) ) ;
#1857=DIRECTION ( 'NONE',  ( -0.000000000000000000, -0.000000000000000000, -1.000000000000000000 ) ) ;
#1859=EDGE_LOOP ( 'NONE', ( #4915, #6008, #2084, #3850 ) ) ;
#1864=CARTESIAN_POINT ( 'NONE',  ( -12.54049055679406344, 29.87738611749458428, 9.974675204776749737 ) ) ;
#1866=DIRECTION ( 'NONE',  ( -0.000000000000000000, -0.000000000000000000, -1.000000000000000000 ) ) ;
#1874=ORIENTED_EDGE ( 'NONE', *, *, #2934, .F. ) ;
#1878=ADVANCED_FACE ( 'NONE', ( #4424 ), #5915, .F. ) ;
#1884=DIRECTION ( 'NONE',  ( -0.000000000000000000, -0.000000000000000000, -1.000000000000000000 ) ) ;
#1888=CYLINDRICAL_SURFACE ( 'NONE', #3173, 166.8359700257217071 ) ;
#1891=ADVANCED_FACE ( 'NONE', ( #5425, #3488 ), #5883, .T. ) ;
#1893=CARTESIAN_POINT ( 'NONE',  ( 174.7835321302054865, 68.75545066608756883, 9.999999999999996447 ) ) ;
#1894=CARTESIAN_POINT ( 'NONE',  ( -12.47915588485122917, 30.13418267071338263, 9.999999999999991118 ) ) ;
#1906=VERTEX_POINT ( 'NONE', #2901 ) ;
#1912=DIRECTION ( 'NONE',  ( -0.000000000000000000, -0.000000000000000000, -1.000000000000000000 ) ) ;
#1930=DIRECTION ( 'NONE',  ( 0.000000000000000000, 1.000000000000000000, -0.000000000000000000 ) ) ;
#1934=ORIENTED_EDGE ( 'NONE', *, *, #4837, .F. ) ;
#1935=FACE_OUTER_BOUND ( 'NONE', #2276, .T. ) ;
#1938=CARTESIAN_POINT ( 'NONE',  ( -17.05141243254543681, 0.000000000000000000, 12.00000000000000000 ) ) ;
#1945=AXIS2_PLACEMENT_3D ( 'NONE', #4470, #5478, #2920 ) ;
#1959=LINE ( 'NONE', #2405, #6056 ) ;
#1965=PLANE ( 'NONE',  #3668 ) ;
#1971=CIRCLE ( 'NONE', #4743, 6.500000000000005329 ) ;
#1974=CARTESIAN_POINT ( 'NONE',  ( -13.41482486054668044, 26.39531364385071299, 5.999999999999990230 ) ) ;
#1987=CARTESIAN_POINT ( 'NONE',  ( 13.27343467285273171, 26.93736435430922072, 3.972397629097673022 ) ) ;
#1988=CARTESIAN_POINT ( 'NONE',  ( 16.00000000000000355, 1.959434878635765526E-15, -4.000000000000000000 ) ) ;
#1991=ORIENTED_EDGE ( 'NONE', *, *, #473, .F. ) ;
#1999=DIRECTION ( 'NONE',  ( -0.000000000000000000, 0.000000000000000000, -1.000000000000000000 ) ) ;
#2003=ORIENTED_EDGE ( 'NONE', *, *, #6291, .F. ) ;
#2013=VERTEX_POINT ( 'NONE', #2187 ) ;
#2016=AXIS2_PLACEMENT_3D ( 'NONE', #3442, #428, #2384 ) ;
#2022=VECTOR ( 'NONE', #2820, 1000.000000000000000 ) ;
#2027=VERTEX_POINT ( 'NONE', #4144 ) ;
#2028=PLANE ( 'NONE',  #3585 ) ;
#2035=DIRECTION ( 'NONE',  ( 0.000000000000000000, -1.000000000000000000, -1.247733429937938623E-16 ) ) ;
#2036=VERTEX_POINT ( 'NONE', #757 ) ;
#2043=ORIENTED_EDGE ( 'NONE', *, *, #315, .T. ) ;
#2065=AXIS2_PLACEMENT_3D ( 'NONE', #1893, #3851, #3360 ) ;
#2076=CYLINDRICAL_SURFACE ( 'NONE', #4374, 4.000000000000000000 ) ;
#2083=DIRECTION ( 'NONE',  ( -0.000000000000000000, 0.000000000000000000, 1.000000000000000000 ) ) ;
#2084=ORIENTED_EDGE ( 'NONE', *, *, #2349, .F. ) ;
#2098=CARTESIAN_POINT ( 'NONE',  ( -6.500000000000000000, 130.6770782520313219, 12.00000000000000000 ) ) ;
#2104=DIRECTION ( 'NONE',  ( -0.000000000000000000, 0.000000000000000000, 1.000000000000000000 ) ) ;
#2108=ORIENTED_EDGE ( 'NONE', *, *, #6223, .F. ) ;
#2122=ORIENTED_EDGE ( 'NONE', *, *, #1493, .T. ) ;
#2123=EDGE_CURVE ( 'NONE', #1293, #4159, #1812, .T. ) ;
#2128=DIRECTION ( 'NONE',  ( -0.000000000000000000, -0.000000000000000000, -1.000000000000000000 ) ) ;
#2130=VERTEX_POINT ( 'NONE', #5905 ) ;
#2139=ORIENTED_EDGE ( 'NONE', *, *, #607, .T. ) ;
#2143=VERTEX_POINT ( 'NONE', #973 ) ;
#2144=VECTOR ( 'NONE', #1022, 1000.000000000000000 ) ;
#2148=AXIS2_PLACEMENT_3D ( 'NONE', #5978, #2976, #4998 ) ;
#2152=VECTOR ( 'NONE', #3483, 1000.000000000000000 ) ;
#2154=ORIENTED_EDGE ( 'NONE', *, *, #700, .F. ) ;
#2165=ORIENTED_EDGE ( 'NONE', *, *, #974, .T. ) ;
#2176=ORIENTED_EDGE ( 'NONE', *, *, #315, .F. ) ;
#2187=CARTESIAN_POINT ( 'NONE',  ( -21.00000000000000355, 0.000000000000000000, 16.00000000000000000 ) ) ;
#2191=ORIENTED_EDGE ( 'NONE', *, *, #1640, .F. ) ;
#2193=ADVANCED_FACE ( 'NONE', ( #4415 ), #881, .F. ) ;
#2197=EDGE_CURVE ( 'NONE', #4930, #643, #3345, .T. ) ;
#2199=DIRECTION ( 'NONE',  ( -0.000000000000000000, -0.000000000000000000, -1.000000000000000000 ) ) ;
#2202=ORIENTED_EDGE ( 'NONE', *, *, #2385, .F. ) ;
#2219=VECTOR ( 'NONE', #4875, 1000.000000000000000 ) ;
#2226=AXIS2_PLACEMENT_3D ( 'NONE', #3438, #3406, #5523 ) ;
#2230=VECTOR ( 'NONE', #3613, 1000.000000000000000 ) ;
#2231=VERTEX_POINT ( 'NONE', #2351 ) ;
#2242=DIRECTION ( 'NONE',  ( 0.000000000000000000, 0.000000000000000000, 1.000000000000000000 ) ) ;
#2243=DIRECTION ( 'NONE',  ( -1.000000000000000000, 1.852483853906148040E-16, 0.000000000000000000 ) ) ;
#2248=AXIS2_PLACEMENT_3D ( 'NONE', #1270, #1785, #3231 ) ;
#2263=DIRECTION ( 'NONE',  ( 1.734723475976809855E-15, 1.000000000000000000, 0.000000000000000000 ) ) ;
#2269=VECTOR ( 'NONE', #381, 1000.000000000000000 ) ;
#2272=EDGE_CURVE ( 'NONE', #4999, #643, #135, .T. ) ;
#2276=EDGE_LOOP ( 'NONE', ( #2997, #2928 ) ) ;
#2279=CARTESIAN_POINT ( 'NONE',  ( 13.41482486054668399, 26.39531364385071655, 5.999999999999990230 ) ) ;
#2288=FACE_OUTER_BOUND ( 'NONE', #1082, .T. ) ;
#2291=EDGE_LOOP ( 'NONE', ( #5282, #5055, #3185, #1207 ) ) ;
#2300=ORIENTED_EDGE ( 'NONE', *, *, #4480, .T. ) ;
#2340=CARTESIAN_POINT ( 'NONE',  ( -12.41746183823000393, 30.39531364385071655, 9.999999999999991118 ) ) ;
#2345=LINE ( 'NONE', #4698, #2837 ) ;
#2349=EDGE_CURVE ( 'NONE', #643, #4930, #5313, .T. ) ;
#2351=CARTESIAN_POINT ( 'NONE',  ( 8.000000000000007105, 72.93807001241029297, 9.999999999999996447 ) ) ;
#2359=VECTOR ( 'NONE', #3620, 1000.000000000000000 ) ;
#2365=CARTESIAN_POINT ( 'NONE',  ( -12.41746183823000393, 30.39531364385071299, 1.999999999999990008 ) ) ;
#2373=AXIS2_PLACEMENT_3D ( 'NONE', #2402, #6308, #2910 ) ;
#2384=DIRECTION ( 'NONE',  ( 1.000000000000000000, 0.000000000000000000, 0.000000000000000000 ) ) ;
#2385=EDGE_CURVE ( 'NONE', #3758, #5846, #6129, .T. ) ;
#2395=AXIS2_PLACEMENT_3D ( 'NONE', #1492, #1884, #5397 ) ;
#2397=CARTESIAN_POINT ( 'NONE',  ( 8.000000000000003553, 100.3953136438507272, 1.999999999999998224 ) ) ;
#2398=EDGE_CURVE ( 'NONE', #5912, #4340, #3774, .T. ) ;
#2402=CARTESIAN_POINT ( 'NONE',  ( 0.000000000000000000, 0.000000000000000000, 16.00000000000000000 ) ) ;
#2405=CARTESIAN_POINT ( 'NONE',  ( 17.05141243254541550, -24.25762350764758679, 12.00000000000000000 ) ) ;
#2406=ORIENTED_EDGE ( 'NONE', *, *, #2776, .F. ) ;
#2420=CARTESIAN_POINT ( 'NONE',  ( 13.05961095629095503, 27.77190499716703798, 9.030829679283289835 ) ) ;
#2428=ORIENTED_EDGE ( 'NONE', *, *, #2385, .T. ) ;
#2432=CIRCLE ( 'NONE', #5418, 12.50000000000001421 ) ;
#2435=EDGE_LOOP ( 'NONE', ( #2497, #3811, #4869, #3341 ) ) ;
#2440=DIRECTION ( 'NONE',  ( -0.000000000000000000, -0.000000000000000000, -1.000000000000000000 ) ) ;
#2447=CARTESIAN_POINT ( 'NONE',  ( -13.38023260448825447, 26.52727575619375244, 4.947004611186087253 ) ) ;
#2453=DIRECTION ( 'NONE',  ( -1.000000000000000000, 0.000000000000000000, 0.000000000000000000 ) ) ;
#2459=ORIENTED_EDGE ( 'NONE', *, *, #579, .T. ) ;
#2462=VECTOR ( 'NONE', #2199, 1000.000000000000000 ) ;
#2465=CARTESIAN_POINT ( 'NONE',  ( 0.000000000000000000, 134.5953136438507158, 12.00000000000000000 ) ) ;
#2476=CIRCLE ( 'NONE', #5781, 166.8359700257217071 ) ;
#2478=ORIENTED_EDGE ( 'NONE', *, *, #187, .T. ) ;
#2489=CARTESIAN_POINT ( 'NONE',  ( 19.25293315802893801, 8.385974291188240670, 12.00000000000000000 ) ) ;
#2492=FACE_BOUND ( 'NONE', #1284, .T. ) ;
#2494=CARTESIAN_POINT ( 'NONE',  ( 7.947562104483774093, 68.75545066608756883, 9.999999999999996447 ) ) ;
#2497=ORIENTED_EDGE ( 'NONE', *, *, #4758, .F. ) ;
#2500=CARTESIAN_POINT ( 'NONE',  ( 0.000000000000000000, 120.0000000000000000, 12.00000000000000000 ) ) ;
#2508=EDGE_CURVE ( 'NONE', #4629, #4930, #3797, .T. ) ;
#2516=LINE ( 'NONE', #5848, #2879 ) ;
#2521=EDGE_LOOP ( 'NONE', ( #4233, #4816, #3843, #1677, #800, #6297, #3877, #2191, #3860 ) ) ;
#2525=DIRECTION ( 'NONE',  ( -1.000000000000000000, -1.852483853906148286E-16, 0.000000000000000000 ) ) ;
#2527=CIRCLE ( 'NONE', #3561, 166.8359700257217071 ) ;
#2540=EDGE_CURVE ( 'NONE', #5896, #2231, #4336, .T. ) ;
#2547=EDGE_CURVE ( 'NONE', #1278, #3016, #1820, .T. ) ;
#2554=ORIENTED_EDGE ( 'NONE', *, *, #6304, .T. ) ;
#2555=DIRECTION ( 'NONE',  ( -0.000000000000000000, -0.000000000000000000, -1.000000000000000000 ) ) ;
#2565=CARTESIAN_POINT ( 'NONE',  ( 174.7835321302054865, 68.75545066608756883, 9.999999999999996447 ) ) ;
#2568=AXIS2_PLACEMENT_3D ( 'NONE', #4441, #2440, #5963 ) ;
#2573=EDGE_LOOP ( 'NONE', ( #2154, #148, #509, #3829 ) ) ;
#2574=MECHANICAL_DESIGN_GEOMETRIC_PRESENTATION_REPRESENTATION('',(#1761),#5268);
#2578=FACE_BOUND ( 'NONE', #5796, .T. ) ;
#2584=ORIENTED_EDGE ( 'NONE', *, *, #230, .T. ) ;
#2585=ADVANCED_FACE ( 'NONE', ( #3433 ), #4367, .T. ) ;
#2592=DIRECTION ( 'NONE',  ( 2.295390878742131754E-32, -1.239088197126290570E-16, 1.000000000000000000 ) ) ;
#2594=FACE_OUTER_BOUND ( 'NONE', #5822, .T. ) ;
#2598=SHAPE_DEFINITION_REPRESENTATION ( #2659, #3711 ) ;
#2604=PLANE ( 'NONE',  #5275 ) ;
#2615=DIRECTION ( 'NONE',  ( 1.000000000000000000, 0.000000000000000000, 0.000000000000000000 ) ) ;
#2616=CARTESIAN_POINT ( 'NONE',  ( 0.000000000000000000, 0.000000000000000000, 12.00000000000000000 ) ) ;
#2631=DIRECTION ( 'NONE',  ( 1.000000000000000000, 0.000000000000000000, 0.000000000000000000 ) ) ;
#2633=DIRECTION ( 'NONE',  ( 0.000000000000000000, 0.000000000000000000, 1.000000000000000000 ) ) ;
#2656=EDGE_CURVE ( 'NONE', #990, #3225, #3167, .T. ) ;
#2659=PRODUCT_DEFINITION_SHAPE ( 'NONE', 'NONE',  #1341 ) ;
#2665=DIRECTION ( 'NONE',  ( 1.000000000000000000, 0.000000000000000000, -0.000000000000000000 ) ) ;
#2671=CARTESIAN_POINT ( 'NONE',  ( 12.50000000000000355, 120.0000000000000000, 12.00000000000000000 ) ) ;
#2676=CARTESIAN_POINT ( 'NONE',  ( -17.05141243254543681, -12.25762350764760455, 0.000000000000000000 ) ) ;
#2685=ORIENTED_EDGE ( 'NONE', *, *, #548, .F. ) ;
#2689=LINE ( 'NONE', #5501, #1547 ) ;
#2690=ORIENTED_EDGE ( 'NONE', *, *, #2272, .T. ) ;
#2694=FACE_OUTER_BOUND ( 'NONE', #4001, .T. ) ;
#2696=VERTEX_POINT ( 'NONE', #1658 ) ;
#2699=FACE_OUTER_BOUND ( 'NONE', #1859, .T. ) ;
#2702=FACE_OUTER_BOUND ( 'NONE', #277, .T. ) ;
#2703=EDGE_LOOP ( 'NONE', ( #2908, #326, #5490, #5307 ) ) ;
#2711=LINE ( 'NONE', #6138, #2748 ) ;
#2719=DIRECTION ( 'NONE',  ( 1.000000000000000000, 0.000000000000000000, 0.000000000000000000 ) ) ;
#2720=FACE_BOUND ( 'NONE', #618, .T. ) ;
#2725=CARTESIAN_POINT ( 'NONE',  ( 0.000000000000000000, 120.0000000000000000, 12.00000000000000000 ) ) ;
#2729=ADVANCED_FACE ( 'NONE', ( #314, #4193 ), #1236, .T. ) ;
#2734=EDGE_CURVE ( 'NONE', #5912, #3044, #1199, .T. ) ;
#2743=CARTESIAN_POINT ( 'NONE',  ( 0.000000000000000000, 120.0000000000000000, 12.00000000000000000 ) ) ;
#2744=VECTOR ( 'NONE', #6293, 1000.000000000000000 ) ;
#2748=VECTOR ( 'NONE', #4685, 1000.000000000000000 ) ;
#2755=CARTESIAN_POINT ( 'NONE',  ( 0.000000000000000000, -24.25762350764758679, 0.000000000000000000 ) ) ;
#2756=VECTOR ( 'NONE', #547, 1000.000000000000000 ) ;
#2757=DIRECTION ( 'NONE',  ( 1.000000000000000000, 0.000000000000000000, 0.000000000000000000 ) ) ;
#2760=CARTESIAN_POINT ( 'NONE',  ( 16.00000000000000355, 1.959434878635765526E-15, 16.00000000000000000 ) ) ;
#2761=VECTOR ( 'NONE', #1336, 1000.000000000000000 ) ;
#2776=EDGE_CURVE ( 'NONE', #2027, #4920, #4418, .T. ) ;
#2779=EDGE_LOOP ( 'NONE', ( #471, #5368, #3902, #1809 ) ) ;
#2791=ORIENTED_EDGE ( 'NONE', *, *, #4137, .T. ) ;
#2801=EDGE_LOOP ( 'NONE', ( #5037, #2685, #5331, #3655 ) ) ;
#2804=CARTESIAN_POINT ( 'NONE',  ( 6.500000000000000000, 130.6770782520313219, 12.00000000000000000 ) ) ;
#2807=VERTEX_POINT ( 'NONE', #3323 ) ;
#2817=CARTESIAN_POINT ( 'NONE',  ( -12.66240722304475774, 29.37208741619406993, 9.875474163642433467 ) ) ;
#2819=ORIENTED_EDGE ( 'NONE', *, *, #187, .F. ) ;
#2820=DIRECTION ( 'NONE',  ( -0.000000000000000000, -0.000000000000000000, -1.000000000000000000 ) ) ;
#2828=VECTOR ( 'NONE', #1602, 1000.000000000000000 ) ;
#2831=VERTEX_POINT ( 'NONE', #2397 ) ;
#2837=VECTOR ( 'NONE', #4214, 1000.000000000000000 ) ;
#2842=DIRECTION ( 'NONE',  ( 0.000000000000000000, 0.000000000000000000, 1.000000000000000000 ) ) ;
#2857=DIRECTION ( 'NONE',  ( 1.000000000000000000, 0.000000000000000000, 0.000000000000000000 ) ) ;
#2859=EDGE_CURVE ( 'NONE', #4159, #1293, #6165, .T. ) ;
#2872=ADVANCED_FACE ( 'NONE', ( #5819 ), #1888, .F. ) ;
#2873=CARTESIAN_POINT ( 'NONE',  ( -6.500000000000000000, 130.6770782520313219, 12.00000000000000000 ) ) ;
#2879=VECTOR ( 'NONE', #3992, 1000.000000000000000 ) ;
#2884=CIRCLE ( 'NONE', #2373, 16.00000000000000355 ) ;
#2887=DIRECTION ( 'NONE',  ( -0.000000000000000000, 0.000000000000000000, 1.000000000000000000 ) ) ;
#2889=CARTESIAN_POINT ( 'NONE',  ( 0.000000000000000000, 0.000000000000000000, 12.00000000000000000 ) ) ;
#2891=DIRECTION ( 'NONE',  ( 0.000000000000000000, -0.000000000000000000, 1.000000000000000000 ) ) ;
#2897=FACE_OUTER_BOUND ( 'NONE', #6030, .T. ) ;
#2899=LINE ( 'NONE', #318, #6263 ) ;
#2901=CARTESIAN_POINT ( 'NONE',  ( -17.05141243254543681, -24.25762350764758679, 12.00000000000000000 ) ) ;
#2902=CYLINDRICAL_SURFACE ( 'NONE', #5001, 16.00000000000000000 ) ;
#2905=DIRECTION ( 'NONE',  ( 1.000000000000000000, 0.000000000000000000, 0.000000000000000000 ) ) ;
#2908=ORIENTED_EDGE ( 'NONE', *, *, #5625, .F. ) ;
#2910=DIRECTION ( 'NONE',  ( 1.000000000000000000, 0.000000000000000000, 0.000000000000000000 ) ) ;
#2919=ORIENTED_EDGE ( 'NONE', *, *, #2123, .T. ) ;
#2920=DIRECTION ( 'NONE',  ( 0.000000000000000000, -1.000000000000000000, 0.000000000000000000 ) ) ;
#2922=DIRECTION ( 'NONE',  ( -1.000000000000000000, 0.000000000000000000, 0.000000000000000000 ) ) ;
#2928=ORIENTED_EDGE ( 'NONE', *, *, #6023, .F. ) ;
#2930=CYLINDRICAL_SURFACE ( 'NONE', #5181, 166.8359700257217071 ) ;
#2931=EDGE_CURVE ( 'NONE', #3745, #1293, #4877, .T. ) ;
#2934=EDGE_CURVE ( 'NONE', #1518, #6319, #4750, .T. ) ;
#2941=ORIENTED_EDGE ( 'NONE', *, *, #5990, .F. ) ;
#2943=ADVANCED_FACE ( 'NONE', ( #6238 ), #1823, .F. ) ;
#2947=LINE ( 'NONE', #5108, #2359 ) ;
#2956=CARTESIAN_POINT ( 'NONE',  ( -8.000000000000003553, 100.3953136438507272, 1.999999999999998224 ) ) ;
#2959=ORIENTED_EDGE ( 'NONE', *, *, #5989, .F. ) ;
#2960=LINE ( 'NONE', #4929, #5765 ) ;
#2965=CARTESIAN_POINT ( 'NONE',  ( -12.47907056128239311, 30.13454381782201352, 1.999999999999989564 ) ) ;
#2973=EDGE_CURVE ( 'NONE', #2143, #4017, #1332, .T. ) ;
#2976=DIRECTION ( 'NONE',  ( -2.295390878742131754E-32, 1.239088197126290570E-16, -1.000000000000000000 ) ) ;
#2977=ORIENTED_EDGE ( 'NONE', *, *, #6307, .F. ) ;
#2987=ORIENTED_EDGE ( 'NONE', *, *, #582, .F. ) ;
#2992=CARTESIAN_POINT ( 'NONE',  ( -17.05141243254543681, 0.000000000000000000, 0.000000000000000000 ) ) ;
#2993=DIRECTION ( 'NONE',  ( 0.000000000000000000, 1.000000000000000000, 0.000000000000000000 ) ) ;
#2994=ORIENTED_EDGE ( 'NONE', *, *, #230, .F. ) ;
#2996=CYLINDRICAL_SURFACE ( 'NONE', #1945, 4.000000000000003553 ) ;
#2997=ORIENTED_EDGE ( 'NONE', *, *, #1626, .F. ) ;
#3002=PLANE ( 'NONE',  #316 ) ;
#3005=CARTESIAN_POINT ( 'NONE',  ( 12.47915588485119898, 30.13418267071338263, 9.999999999999991118 ) ) ;
#3008=CARTESIAN_POINT ( 'NONE',  ( -19.25293315802951000, 8.385974291186927942, 0.000000000000000000 ) ) ;
#3011=ORIENTED_EDGE ( 'NONE', *, *, #946, .T. ) ;
#3016=VERTEX_POINT ( 'NONE', #1069 ) ;
#3017=EDGE_CURVE ( 'NONE', #1786, #2027, #3997, .T. ) ;
#3028=PRODUCT_DEFINITION_FORMATION_WITH_SPECIFIED_SOURCE ( 'ANY', '', #6067, .NOT_KNOWN. ) ;
#3030=ORIENTED_EDGE ( 'NONE', *, *, #3415, .T. ) ;
#3034=DIRECTION ( 'NONE',  ( -1.734723475976809855E-15, -1.000000000000000000, 0.000000000000000000 ) ) ;
#3038=AXIS2_PLACEMENT_3D ( 'NONE', #3563, #5532, #1106 ) ;
#3043=DIRECTION ( 'NONE',  ( 1.000000000000000000, 0.000000000000000000, 0.000000000000000000 ) ) ;
#3044=VERTEX_POINT ( 'NONE', #2494 ) ;
#3052=DIRECTION ( 'NONE',  ( -1.852483853906148040E-16, 1.000000000000000000, 0.000000000000000000 ) ) ;
#3054=VERTEX_POINT ( 'NONE', #5950 ) ;
#3057=DIRECTION ( 'NONE',  ( 1.000000000000000000, 0.000000000000000000, 0.000000000000000000 ) ) ;
#3076=CARTESIAN_POINT ( 'NONE',  ( 13.40780655258104836, 26.42202358648260940, 5.467569244659290284 ) ) ;
#3078=CARTESIAN_POINT ( 'NONE',  ( -174.7835321302054865, 68.75545066608756883, 1.999999999999994893 ) ) ;
#3080=LINE ( 'NONE', #5008, #4607 ) ;
#3083=AXIS2_PLACEMENT_3D ( 'NONE', #1704, #5131, #238 ) ;
#3087=DIRECTION ( 'NONE',  ( -0.000000000000000000, 0.000000000000000000, 1.000000000000000000 ) ) ;
#3095=CARTESIAN_POINT ( 'NONE',  ( 0.000000000000000000, 0.000000000000000000, 12.00000000000000000 ) ) ;
#3106=DIRECTION ( 'NONE',  ( -0.000000000000000000, -0.000000000000000000, -1.000000000000000000 ) ) ;
#3114=ORIENTED_EDGE ( 'NONE', *, *, #947, .T. ) ;
#3119=ORIENTED_EDGE ( 'NONE', *, *, #1539, .T. ) ;
#3126=EDGE_LOOP ( 'NONE', ( #3924, #1318, #4052, #5422 ) ) ;
#3132=DIRECTION ( 'NONE',  ( 0.000000000000000000, -0.000000000000000000, -1.000000000000000000 ) ) ;
#3143=ORIENTED_EDGE ( 'NONE', *, *, #2349, .T. ) ;
#3150=CARTESIAN_POINT ( 'NONE',  ( 7.947562104483774093, 68.75545066608756883, 12.00000000000000000 ) ) ;
#3152=VERTEX_POINT ( 'NONE', #2098 ) ;
#3166=VECTOR ( 'NONE', #4650, 1000.000000000000000 ) ;
#3167=LINE ( 'NONE', #3621, #5002 ) ;
#3168=LINE ( 'NONE', #737, #3166 ) ;
#3170=CIRCLE ( 'NONE', #4926, 166.8359700257217071 ) ;
#3173=AXIS2_PLACEMENT_3D ( 'NONE', #3847, #5241, #828 ) ;
#3177=DIRECTION ( 'NONE',  ( -1.000000000000000000, 0.000000000000000000, 0.000000000000000000 ) ) ;
#3185=ORIENTED_EDGE ( 'NONE', *, *, #6023, .T. ) ;
#3187=DIRECTION ( 'NONE',  ( -0.000000000000000000, -0.000000000000000000, -1.000000000000000000 ) ) ;
#3195=CARTESIAN_POINT ( 'NONE',  ( -19.25293315802950644, 8.385974291186926166, 12.00000000000000000 ) ) ;
#3206=EDGE_LOOP ( 'NONE', ( #6100, #574, #4437, #2919 ) ) ;
#3214=FACE_OUTER_BOUND ( 'NONE', #3206, .T. ) ;
#3223=DIRECTION ( 'NONE',  ( 1.000000000000000000, 0.000000000000000000, -0.000000000000000000 ) ) ;
#3224=LINE ( 'NONE', #1129, #5253 ) ;
#3225=VERTEX_POINT ( 'NONE', #2676 ) ;
#3226=EDGE_LOOP ( 'NONE', ( #1051, #4545, #2690, #1039 ) ) ;
#3231=DIRECTION ( 'NONE',  ( 1.000000000000000000, 0.000000000000000000, 0.000000000000000000 ) ) ;
#3245=EDGE_CURVE ( 'NONE', #3758, #5734, #3224, .T. ) ;
#3246=LINE ( 'NONE', #2992, #1248 ) ;
#3255=ADVANCED_FACE ( 'NONE', ( #2702 ), #4085, .F. ) ;
#3256=VECTOR ( 'NONE', #1912, 1000.000000000000000 ) ;
#3270=ORIENTED_EDGE ( 'NONE', *, *, #2931, .F. ) ;
#3279=B_SPLINE_CURVE_WITH_KNOTS ( 'NONE', 3,
 ( #1974, #3512, #4378, #2447, #5364, #975, #4417, #10, #495, #456, #5393, #5419, #3937, #4966, #5910, #1458, #2965, #558 ),
 .UNSPECIFIED., .F., .F.,
 ( 4, 2, 2, 2, 2, 2, 2, 2, 4 ),
 ( 0.006348828280262476358, 0.007141278029982640538, 0.007933727779702805585, 0.008726177529422968898, 0.009518627279143133946, 0.01031107702886330073, 0.01110352677858346578, 0.01189597652830363256, 0.01268842627802379761 ),
 .UNSPECIFIED. ) ;
#3280=DIRECTION ( 'NONE',  ( -0.000000000000000000, -0.000000000000000000, -1.000000000000000000 ) ) ;
#3294=CIRCLE ( 'NONE', #4430, 4.000000000000003553 ) ;
#3298=CARTESIAN_POINT ( 'NONE',  ( 17.05141243254543681, -12.25762350764760455, 12.00000000000000000 ) ) ;
#3308=CARTESIAN_POINT ( 'NONE',  ( 174.7835321302054865, 68.75545066608756883, 0.000000000000000000 ) ) ;
#3309=LINE ( 'NONE', #4305, #22 ) ;
#3312=ORIENTED_EDGE ( 'NONE', *, *, #1584, .T. ) ;
#3322=FACE_OUTER_BOUND ( 'NONE', #6331, .T. ) ;
#3323=CARTESIAN_POINT ( 'NONE',  ( -8.000000000000007105, 72.93807001241029297, 1.999999999999974021 ) ) ;
#3325=ORIENTED_EDGE ( 'NONE', *, *, #3898, .T. ) ;
#3328=DIRECTION ( 'NONE',  ( -1.734723475976809855E-15, -1.000000000000000000, 0.000000000000000000 ) ) ;
#3329=CARTESIAN_POINT ( 'NONE',  ( -13.19716647944431642, 27.23303957064661418, 8.463596398456378012 ) ) ;
#3330=ADVANCED_FACE ( 'NONE', ( #2897 ), #4475, .T. ) ;
#3341=ORIENTED_EDGE ( 'NONE', *, *, #1626, .T. ) ;
#3345=CIRCLE ( 'NONE', #2016, 16.00000000000000355 ) ;
#3346=LINE ( 'NONE', #1814, #2744 ) ;
#3348=ORIENTED_EDGE ( 'NONE', *, *, #2734, .T. ) ;
#3350=ORIENTED_EDGE ( 'NONE', *, *, #2547, .T. ) ;
#3351=DIRECTION ( 'NONE',  ( 1.000000000000000000, 0.000000000000000000, -0.000000000000000000 ) ) ;
#3352=LINE ( 'NONE', #2873, #3256 ) ;
#3353=CIRCLE ( 'NONE', #86, 12.50000000000001421 ) ;
#3358=AXIS2_PLACEMENT_3D ( 'NONE', #3663, #1250, #5120 ) ;
#3360=DIRECTION ( 'NONE',  ( 0.000000000000000000, 1.000000000000000000, 1.247733429937938623E-16 ) ) ;
#3361=APPLICATION_CONTEXT ( 'automotive_design' ) ;
#3380=DIRECTION ( 'NONE',  ( -0.000000000000000000, -0.000000000000000000, -1.000000000000000000 ) ) ;
#3382=AXIS2_PLACEMENT_3D ( 'NONE', #3757, #468, #5722 ) ;
#3390=DIRECTION ( 'NONE',  ( 0.000000000000000000, 0.000000000000000000, 1.000000000000000000 ) ) ;
#3391=DIRECTION ( 'NONE',  ( 1.000000000000000000, -1.734723475976809855E-15, 0.000000000000000000 ) ) ;
#3395=EDGE_LOOP ( 'NONE', ( #106, #695, #2819, #3939, #3030, #386, #5694, #2791 ) ) ;
#3400=CIRCLE ( 'NONE', #5054, 21.00000000000000355 ) ;
#3403=ADVANCED_FACE ( 'NONE', ( #5454 ), #3002, .T. ) ;
#3404=DIRECTION ( 'NONE',  ( 1.852483853906148040E-16, -1.000000000000000000, -1.239088197126290570E-16 ) ) ;
#3406=DIRECTION ( 'NONE',  ( -0.000000000000000000, 0.000000000000000000, 1.000000000000000000 ) ) ;
#3415=EDGE_CURVE ( 'NONE', #2696, #4920, #5911, .T. ) ;
#3433=FACE_OUTER_BOUND ( 'NONE', #3537, .T. ) ;
#3438=CARTESIAN_POINT ( 'NONE',  ( -174.7835321302054865, 68.75545066608756883, 12.00000000000000000 ) ) ;
#3442=CARTESIAN_POINT ( 'NONE',  ( 0.000000000000000000, 0.000000000000000000, -4.000000000000000000 ) ) ;
#3443=ADVANCED_FACE ( 'NONE', ( #4663 ), #5025, .F. ) ;
#3446=DIRECTION ( 'NONE',  ( 1.000000000000000000, 0.000000000000000000, 0.000000000000000000 ) ) ;
#3447=ORIENTED_EDGE ( 'NONE', *, *, #946, .F. ) ;
#3451=AXIS2_PLACEMENT_3D ( 'NONE', #493, #4802, #2857 ) ;
#3458=ORIENTED_EDGE ( 'NONE', *, *, #5527, .T. ) ;
#3460=VERTEX_POINT ( 'NONE', #5124 ) ;
#3464=ORIENTED_EDGE ( 'NONE', *, *, #3943, .T. ) ;
#3465=CARTESIAN_POINT ( 'NONE',  ( 12.72367524380681658, 29.12081030169099805, 2.199628915743095714 ) ) ;
#3481=AXIS2_PLACEMENT_3D ( 'NONE', #1624, #2525, #3590 ) ;
#3483=DIRECTION ( 'NONE',  ( -1.852483853906148040E-16, 1.000000000000000000, 0.000000000000000000 ) ) ;
#3484=ORIENTED_EDGE ( 'NONE', *, *, #3245, .T. ) ;
#3487=CARTESIAN_POINT ( 'NONE',  ( 13.40794989232620615, 26.42147665086397623, 6.529465147186706453 ) ) ;
#3488=FACE_BOUND ( 'NONE', #1375, .T. ) ;
#3498=CARTESIAN_POINT ( 'NONE',  ( 12.41746183822997551, 30.39531364385071299, 1.999999999999990008 ) ) ;
#3499=CARTESIAN_POINT ( 'NONE',  ( 0.000000000000000000, 0.000000000000000000, 0.000000000000000000 ) ) ;
#3509=EDGE_LOOP ( 'NONE', ( #2108, #6332, #1265, #2300, #2478, #1634, #6173 ) ) ;
#3510=DIRECTION ( 'NONE',  ( 0.000000000000000000, 0.000000000000000000, 1.000000000000000000 ) ) ;
#3512=CARTESIAN_POINT ( 'NONE',  ( -13.41482486054669465, 26.39531364385071655, 5.735664331006448791 ) ) ;
#3527=EDGE_CURVE ( 'NONE', #2013, #823, #3700, .T. ) ;
#3537=EDGE_LOOP ( 'NONE', ( #6041, #1708, #2043, #4880 ) ) ;
#3547=DIRECTION ( 'NONE',  ( -2.295390878742131754E-32, 1.239088197126290570E-16, -1.000000000000000000 ) ) ;
#3551=VERTEX_POINT ( 'NONE', #426 ) ;
#3552=ORIENTED_EDGE ( 'NONE', *, *, #5288, .F. ) ;
#3556=CARTESIAN_POINT ( 'NONE',  ( 13.41482486054666268, 26.39531364385071299, 5.735664331006449679 ) ) ;
#3561=AXIS2_PLACEMENT_3D ( 'NONE', #6168, #3132, #826 ) ;
#3563=CARTESIAN_POINT ( 'NONE',  ( -174.7835321302054865, 68.75545066608756883, 0.000000000000000000 ) ) ;
#3565=ORIENTED_EDGE ( 'NONE', *, *, #3943, .F. ) ;
#3584=DIRECTION ( 'NONE',  ( 0.000000000000000000, 0.000000000000000000, 1.000000000000000000 ) ) ;
#3585=AXIS2_PLACEMENT_3D ( 'NONE', #5965, #3510, #1057 ) ;
#3586=CARTESIAN_POINT ( 'NONE',  ( 12.84176997259613273, 28.64101934588368081, 2.395886979664402894 ) ) ;
#3590=DIRECTION ( 'NONE',  ( 0.000000000000000000, -1.000000000000000000, 0.000000000000000000 ) ) ;
#3599=DIRECTION ( 'NONE',  ( 1.000000000000000000, 0.000000000000000000, 0.000000000000000000 ) ) ;
#3605=ORIENTED_EDGE ( 'NONE', *, *, #4837, .T. ) ;
#3607=DIRECTION ( 'NONE',  ( 1.000000000000000000, 0.000000000000000000, 0.000000000000000000 ) ) ;
#3613=DIRECTION ( 'NONE',  ( -1.000000000000000000, -1.852483853906148286E-16, 0.000000000000000000 ) ) ;
#3620=DIRECTION ( 'NONE',  ( -1.000000000000000000, -1.852483853906148286E-16, 0.000000000000000000 ) ) ;
#3621=CARTESIAN_POINT ( 'NONE',  ( -17.05141243254543681, -12.25762350764760455, 12.00000000000000000 ) ) ;
#3627=FACE_OUTER_BOUND ( 'NONE', #1218, .T. ) ;
#3630=( NAMED_UNIT ( * ) PLANE_ANGLE_UNIT ( ) SI_UNIT ( $, .RADIAN. ) );
#3632=LINE ( 'NONE', #5603, #3678 ) ;
#3637=LINE ( 'NONE', #398, #4527 ) ;
#3639=DIRECTION ( 'NONE',  ( 1.852483853906148040E-16, -1.000000000000000000, 0.000000000000000000 ) ) ;
#3647=DIRECTION ( 'NONE',  ( 0.000000000000000000, 1.000000000000000000, -0.000000000000000000 ) ) ;
#3649=CARTESIAN_POINT ( 'NONE',  ( 7.947562104483774093, 68.75545066608756883, 12.00000000000000000 ) ) ;
#3655=ORIENTED_EDGE ( 'NONE', *, *, #1449, .T. ) ;
#3661=AXIS2_PLACEMENT_3D ( 'NONE', #876, #4662, #256 ) ;
#3663=CARTESIAN_POINT ( 'NONE',  ( 0.000000000000000000, 0.000000000000000000, 0.000000000000000000 ) ) ;
#3668=AXIS2_PLACEMENT_3D ( 'NONE', #5354, #4860, #902 ) ;
#3670=( LENGTH_UNIT ( ) NAMED_UNIT ( * ) SI_UNIT ( .MILLI., .METRE. ) );
#3678=VECTOR ( 'NONE', #1182, 1000.000000000000000 ) ;
#3685=ADVANCED_FACE ( 'NONE', ( #5448, #5356 ), #525, .T. ) ;
#3688=EDGE_CURVE ( 'NONE', #2831, #5896, #3294, .T. ) ;
#3689=AXIS2_PLACEMENT_3D ( 'NONE', #2725, #5164, #3607 ) ;
#3691=ADVANCED_FACE ( 'NONE', ( #1029 ), #3959, .F. ) ;
#3692=DIRECTION ( 'NONE',  ( 1.000000000000000000, 0.000000000000000000, 0.000000000000000000 ) ) ;
#3694=ORIENTED_EDGE ( 'NONE', *, *, #5902, .F. ) ;
#3700=CIRCLE ( 'NONE', #3704, 21.00000000000000355 ) ;
#3702=PLANE ( 'NONE',  #3724 ) ;
#3704=AXIS2_PLACEMENT_3D ( 'NONE', #651, #1804, #4796 ) ;
#3706=ORIENTED_EDGE ( 'NONE', *, *, #4270, .T. ) ;
#3711=SHAPE_REPRESENTATION ( 'Part 32,5_Varsay\X2\0131\X0\lan', ( #6349 ), #596 ) ;
#3715=VECTOR ( 'NONE', #3328, 1000.000000000000000 ) ;
#3722=LINE ( 'NONE', #4583, #4827 ) ;
#3724=AXIS2_PLACEMENT_3D ( 'NONE', #1251, #2243, #3740 ) ;
#3740=DIRECTION ( 'NONE',  ( -1.852483853906148040E-16, -1.000000000000000000, 0.000000000000000000 ) ) ;
#3742=ADVANCED_FACE ( 'NONE', ( #193 ), #4106, .F. ) ;
#3745=VERTEX_POINT ( 'NONE', #5117 ) ;
#3749=CARTESIAN_POINT ( 'NONE',  ( -6.500000000000005329, 120.0000000000000000, -4.000000000000000000 ) ) ;
#3757=CARTESIAN_POINT ( 'NONE',  ( 0.000000000000000000, 120.0000000000000000, -4.000000000000000000 ) ) ;
#3758=VERTEX_POINT ( 'NONE', #1692 ) ;
#3774=CIRCLE ( 'NONE', #1296, 166.8359700257217071 ) ;
#3791=FACE_OUTER_BOUND ( 'NONE', #3395, .T. ) ;
#3792=CARTESIAN_POINT ( 'NONE',  ( -8.000000000000021316, 1.481987083124922376E-15, 0.000000000000000000 ) ) ;
#3797=LINE ( 'NONE', #5287, #2022 ) ;
#3811=ORIENTED_EDGE ( 'NONE', *, *, #3527, .F. ) ;
#3816=CARTESIAN_POINT ( 'NONE',  ( 17.05141243254541550, -24.25762350764758679, 12.00000000000000000 ) ) ;
#3825=CARTESIAN_POINT ( 'NONE',  ( -13.00740645622773606, 27.97830129128178811, 9.197704556789860320 ) ) ;
#3829=ORIENTED_EDGE ( 'NONE', *, *, #548, .T. ) ;
#3843=ORIENTED_EDGE ( 'NONE', *, *, #4859, .T. ) ;
#3847=CARTESIAN_POINT ( 'NONE',  ( 174.7835321302054865, 68.75545066608756883, 12.00000000000000000 ) ) ;
#3848=ORIENTED_EDGE ( 'NONE', *, *, #521, .T. ) ;
#3850=ORIENTED_EDGE ( 'NONE', *, *, #2272, .F. ) ;
#3851=DIRECTION ( 'NONE',  ( 2.295390878742131754E-32, -1.239088197126290570E-16, 1.000000000000000000 ) ) ;
#3852=CARTESIAN_POINT ( 'NONE',  ( -12.84201764556569536, 28.64001483306500617, 9.603681688880101319 ) ) ;
#3854=ORIENTED_EDGE ( 'NONE', *, *, #5146, .F. ) ;
#3860=ORIENTED_EDGE ( 'NONE', *, *, #6291, .T. ) ;
#3861=AXIS2_PLACEMENT_3D ( 'NONE', #5983, #3584, #2615 ) ;
#3867=ORIENTED_EDGE ( 'NONE', *, *, #4064, .F. ) ;
#3872=CIRCLE ( 'NONE', #4814, 6.500000000000005329 ) ;
#3877=ORIENTED_EDGE ( 'NONE', *, *, #1584, .F. ) ;
#3882=ADVANCED_FACE ( 'NONE', ( #3627 ), #4039, .F. ) ;
#3886=AXIS2_PLACEMENT_3D ( 'NONE', #6016, #2083, #3043 ) ;
#3892=DIRECTION ( 'NONE',  ( 1.000000000000000000, -1.852483853906148040E-16, -0.000000000000000000 ) ) ;
#3893=DIRECTION ( 'NONE',  ( 0.000000000000000000, -1.000000000000000000, 0.000000000000000000 ) ) ;
#3896=DIRECTION ( 'NONE',  ( 1.000000000000000000, 0.000000000000000000, -0.000000000000000000 ) ) ;
#3898=EDGE_CURVE ( 'NONE', #4340, #1760, #2689, .T. ) ;
#3902=ORIENTED_EDGE ( 'NONE', *, *, #4886, .F. ) ;
#3908=FACE_OUTER_BOUND ( 'NONE', #3226, .T. ) ;
#3923=DIRECTION ( 'NONE',  ( -0.000000000000000000, -0.000000000000000000, -1.000000000000000000 ) ) ;
#3924=ORIENTED_EDGE ( 'NONE', *, *, #4581, .F. ) ;
#3937=CARTESIAN_POINT ( 'NONE',  ( -12.84176997259613096, 28.64101934588367371, 2.395886979664402006 ) ) ;
#3939=ORIENTED_EDGE ( 'NONE', *, *, #1247, .T. ) ;
#3941=CARTESIAN_POINT ( 'NONE',  ( 12.41746183822997551, 30.39531364385071655, 9.999999999999991118 ) ) ;
#3943=EDGE_CURVE ( 'NONE', #4451, #1278, #1727, .T. ) ;
#3952=CARTESIAN_POINT ( 'NONE',  ( 12.89959272829392845, 28.40844700521621036, 2.518705683379065974 ) ) ;
#3959=PLANE ( 'NONE',  #1230 ) ;
#3965=VERTEX_POINT ( 'NONE', #806 ) ;
#3971=CARTESIAN_POINT ( 'NONE',  ( -8.000000000000021316, 2.721075280251214820E-15, 1.999999999999986233 ) ) ;
#3976=AXIS2_PLACEMENT_3D ( 'NONE', #484, #2887, #4856 ) ;
#3977=CARTESIAN_POINT ( 'NONE',  ( 13.30660938351089584, 26.80958678890347713, 4.207676383415306809 ) ) ;
#3992=DIRECTION ( 'NONE',  ( 1.000000000000000000, 0.000000000000000000, 0.000000000000000000 ) ) ;
#3997=LINE ( 'NONE', #5514, #1026 ) ;
#4001=EDGE_LOOP ( 'NONE', ( #1407, #1618, #4208, #2584 ) ) ;
#4003=CARTESIAN_POINT ( 'NONE',  ( 13.19762691892552908, 27.23125096863189754, 3.538843351020406480 ) ) ;
#4004=DIRECTION ( 'NONE',  ( 1.000000000000000000, 0.000000000000000000, 0.000000000000000000 ) ) ;
#4009=ADVANCED_FACE ( 'NONE', ( #870 ), #385, .T. ) ;
#4017=VERTEX_POINT ( 'NONE', #2340 ) ;
#4029=ORIENTED_EDGE ( 'NONE', *, *, #4859, .F. ) ;
#4031=CARTESIAN_POINT ( 'NONE',  ( 18.00000000000001421, 30.39531364385072010, 5.999999999999990230 ) ) ;
#4039=CYLINDRICAL_SURFACE ( 'NONE', #4734, 6.500000000000001776 ) ;
#4043=DIRECTION ( 'NONE',  ( 0.000000000000000000, 0.000000000000000000, 1.000000000000000000 ) ) ;
#4047=LINE ( 'NONE', #2671, #1655 ) ;
#4052=ORIENTED_EDGE ( 'NONE', *, *, #4952, .F. ) ;
#4054=AXIS2_PLACEMENT_3D ( 'NONE', #4203, #1792, #3692 ) ;
#4056=CARTESIAN_POINT ( 'NONE',  ( 8.000000000000000000, 110.3953136438507130, 12.00000000000000000 ) ) ;
#4064=EDGE_CURVE ( 'NONE', #997, #1301, #1959, .T. ) ;
#4081=( NAMED_UNIT ( * ) SI_UNIT ( $, .STERADIAN. ) SOLID_ANGLE_UNIT ( ) );
#4085=CYLINDRICAL_SURFACE ( 'NONE', #3083, 6.500000000000001776 ) ;
#4092=CARTESIAN_POINT ( 'NONE',  ( -6.500000000000000000, 0.000000000000000000, 0.000000000000000000 ) ) ;
#4097=ORIENTED_EDGE ( 'NONE', *, *, #660, .F. ) ;
#4102=CARTESIAN_POINT ( 'NONE',  ( 17.05141243254543681, -12.25762350764760455, 12.00000000000000000 ) ) ;
#4104=ADVANCED_FACE ( 'NONE', ( #4523 ), #185, .F. ) ;
#4106=PLANE ( 'NONE',  #321 ) ;
#4120=VERTEX_POINT ( 'NONE', #5592 ) ;
#4133=CARTESIAN_POINT ( 'NONE',  ( 0.000000000000000000, 120.0000000000000000, 12.00000000000000000 ) ) ;
#4137=EDGE_CURVE ( 'NONE', #4340, #2231, #3080, .T. ) ;
#4144=CARTESIAN_POINT ( 'NONE',  ( -8.000000000000005329, 110.3953136438506988, 0.000000000000000000 ) ) ;
#4147=LINE ( 'NONE', #6036, #2230 ) ;
#4159=VERTEX_POINT ( 'NONE', #6081 ) ;
#4164=ORIENTED_EDGE ( 'NONE', *, *, #5548, .T. ) ;
#4169=DIRECTION ( 'NONE',  ( 1.000000000000000000, 0.000000000000000000, 0.000000000000000000 ) ) ;
#4192=ADVANCED_FACE ( 'NONE', ( #2594 ), #156, .F. ) ;
#4193=FACE_OUTER_BOUND ( 'NONE', #1482, .T. ) ;
#4196=DIRECTION ( 'NONE',  ( 1.852483853906148040E-16, 1.000000000000000000, 0.000000000000000000 ) ) ;
#4203=CARTESIAN_POINT ( 'NONE',  ( 0.000000000000000000, 0.000000000000000000, 16.00000000000000000 ) ) ;
#4208=ORIENTED_EDGE ( 'NONE', *, *, #1367, .F. ) ;
#4212=( LENGTH_UNIT ( ) NAMED_UNIT ( * ) SI_UNIT ( .MILLI., .METRE. ) );
#4214=DIRECTION ( 'NONE',  ( -1.852483853906148040E-16, -1.000000000000000000, -1.239088197126290570E-16 ) ) ;
#4222=DIRECTION ( 'NONE',  ( 0.000000000000000000, 0.000000000000000000, 1.000000000000000000 ) ) ;
#4224=CIRCLE ( 'NONE', #2065, 166.8359700257217071 ) ;
#4229=CARTESIAN_POINT ( 'NONE',  ( 21.00000000000000355, 2.571758278209442056E-15, 16.00000000000000000 ) ) ;
#4230=CARTESIAN_POINT ( 'NONE',  ( 0.000000000000000000, 120.0000000000000000, -4.000000000000000000 ) ) ;
#4231=DIRECTION ( 'NONE',  ( -0.000000000000000000, -0.000000000000000000, -1.000000000000000000 ) ) ;
#4233=ORIENTED_EDGE ( 'NONE', *, *, #4400, .T. ) ;
#4240=VECTOR ( 'NONE', #1819, 1000.000000000000000 ) ;
#4241=LINE ( 'NONE', #2755, #227 ) ;
#4244=EDGE_LOOP ( 'NONE', ( #2459, #5173 ) ) ;
#4255=CARTESIAN_POINT ( 'NONE',  ( 0.000000000000000000, 120.0000000000000000, 16.00000000000000000 ) ) ;
#4261=CARTESIAN_POINT ( 'NONE',  ( -12.41746183823000393, 30.39531364385071655, 9.999999999999991118 ) ) ;
#4263=CARTESIAN_POINT ( 'NONE',  ( 0.000000000000000000, 134.5953136438507158, 12.00000000000000000 ) ) ;
#4270=EDGE_CURVE ( 'NONE', #5794, #5286, #2711, .T. ) ;
#4271=DIRECTION ( 'NONE',  ( 1.000000000000000000, 0.000000000000000000, 0.000000000000000000 ) ) ;
#4277=UNCERTAINTY_MEASURE_WITH_UNIT (LENGTH_MEASURE( 1.000000000000000082E-05 ), #4212, 'distance_accuracy_value', 'NONE');
#4305=CARTESIAN_POINT ( 'NONE',  ( 8.000000000000007105, 72.93807001241029297, 12.00000000000000000 ) ) ;
#4322=DIRECTION ( 'NONE',  ( -0.000000000000000000, -0.000000000000000000, -1.000000000000000000 ) ) ;
#4331=CARTESIAN_POINT ( 'NONE',  ( 0.000000000000000000, 120.0000000000000000, -4.000000000000000000 ) ) ;
#4336=LINE ( 'NONE', #5314, #4585 ) ;
#4337=DIRECTION ( 'NONE',  ( -0.000000000000000000, 0.000000000000000000, 1.000000000000000000 ) ) ;
#4340=VERTEX_POINT ( 'NONE', #912 ) ;
#4361=EDGE_CURVE ( 'NONE', #3965, #1786, #2899, .T. ) ;
#4363=CARTESIAN_POINT ( 'NONE',  ( 8.000000000000021316, 1.481987083124922376E-15, 12.00000000000000000 ) ) ;
#4367=PLANE ( 'NONE',  #3976 ) ;
#4374=AXIS2_PLACEMENT_3D ( 'NONE', #4031, #6076, #1653 ) ;
#4375=FACE_BOUND ( 'NONE', #203, .T. ) ;
#4378=CARTESIAN_POINT ( 'NONE',  ( -13.40780655258107146, 26.42202358648259519, 5.467569244659289396 ) ) ;
#4380=CARTESIAN_POINT ( 'NONE',  ( 0.000000000000000000, 0.000000000000000000, 12.00000000000000000 ) ) ;
#4384=CARTESIAN_POINT ( 'NONE',  ( 13.27340567884428957, 26.93747317953756593, 8.027960515371223238 ) ) ;
#4388=AXIS2_PLACEMENT_3D ( 'NONE', #4408, #3892, #611 ) ;
#4390=LINE ( 'NONE', #3971, #5228 ) ;
#4399=LINE ( 'NONE', #2465, #2144 ) ;
#4400=EDGE_CURVE ( 'NONE', #3965, #2143, #3168, .T. ) ;
#4408=CARTESIAN_POINT ( 'NONE',  ( -8.000000000000003553, 100.3953136438507272, 5.999999999999999112 ) ) ;
#4415=FACE_OUTER_BOUND ( 'NONE', #2779, .T. ) ;
#4417=CARTESIAN_POINT ( 'NONE',  ( -13.27343467285272816, 26.93736435430921716, 3.972397629097670357 ) ) ;
#4418=CIRCLE ( 'NONE', #2248, 12.50000000000001421 ) ;
#4422=B_SPLINE_CURVE_WITH_KNOTS ( 'NONE', 3,
 ( #6013, #3556, #3076, #5076, #4550, #3977, #1987, #4003, #5005, #1500, #666, #3952, #3586, #3465, #5438, #5987, #5042, #3498 ),
 .UNSPECIFIED., .F., .F.,
 ( 4, 2, 2, 2, 2, 2, 2, 2, 4 ),
 ( 0.006348828280262475490, 0.007141278029982640538, 0.007933727779702805585, 0.008726177529422970633, 0.009518627279143135680, 0.01031107702886330073, 0.01110352677858346578, 0.01189597652830363082, 0.01268842627802379587 ),
 .UNSPECIFIED. ) ;
#4423=CARTESIAN_POINT ( 'NONE',  ( 13.19716647944431820, 27.23303957064661773, 8.463596398456379788 ) ) ;
#4424=FACE_OUTER_BOUND ( 'NONE', #831, .T. ) ;
#4430=AXIS2_PLACEMENT_3D ( 'NONE', #1481, #1055, #3893 ) ;
#4437=ORIENTED_EDGE ( 'NONE', *, *, #2931, .T. ) ;
#4441=CARTESIAN_POINT ( 'NONE',  ( 0.000000000000000000, 0.000000000000000000, 12.00000000000000000 ) ) ;
#4447=CARTESIAN_POINT ( 'NONE',  ( 12.41746183822997551, 30.39531364385071299, 1.999999999999990008 ) ) ;
#4448=CARTESIAN_POINT ( 'NONE',  ( 18.00000000000000355, 100.3953136438507272, 1.999999999999998224 ) ) ;
#4451=VERTEX_POINT ( 'NONE', #2489 ) ;
#4457=ORIENTED_EDGE ( 'NONE', *, *, #6177, .F. ) ;
#4460=DIRECTION ( 'NONE',  ( -0.000000000000000000, 0.000000000000000000, 1.000000000000000000 ) ) ;
#4470=CARTESIAN_POINT ( 'NONE',  ( 18.00000000000000355, 100.3953136438507272, 5.999999999999999112 ) ) ;
#4472=DIRECTION ( 'NONE',  ( 1.000000000000000000, 0.000000000000000000, 0.000000000000000000 ) ) ;
#4474=ADVANCED_BREP_SHAPE_REPRESENTATION ( '', ( #151, #6349 ), #596 ) ;
#4475=PLANE ( 'NONE',  #6172 ) ;
#4480=EDGE_CURVE ( 'NONE', #1266, #1008, #3170, .T. ) ;
#4481=LINE ( 'NONE', #5486, #4810 ) ;
#4484=ORIENTED_EDGE ( 'NONE', *, *, #4361, .T. ) ;
#4486=AXIS2_PLACEMENT_3D ( 'NONE', #4255, #3390, #1855 ) ;
#4491=CIRCLE ( 'NONE', #2226, 166.8359700257217071 ) ;
#4498=ORIENTED_EDGE ( 'NONE', *, *, #4480, .F. ) ;
#4501=DIRECTION ( 'NONE',  ( 0.000000000000000000, 0.000000000000000000, 1.000000000000000000 ) ) ;
#4523=FACE_OUTER_BOUND ( 'NONE', #192, .T. ) ;
#4526=DIRECTION ( 'NONE',  ( 2.295390878742131754E-32, -1.239088197126290570E-16, 1.000000000000000000 ) ) ;
#4527=VECTOR ( 'NONE', #5294, 1000.000000000000000 ) ;
#4533=AXIS2_PLACEMENT_3D ( 'NONE', #2889, #4337, #1028 ) ;
#4545=ORIENTED_EDGE ( 'NONE', *, *, #1600, .T. ) ;
#4550=CARTESIAN_POINT ( 'NONE',  ( 13.35991119780008418, 26.60492657425309559, 4.695075907386113911 ) ) ;
#4565=CARTESIAN_POINT ( 'NONE',  ( 0.000000000000000000, 0.000000000000000000, -4.000000000000000000 ) ) ;
#4566=CARTESIAN_POINT ( 'NONE',  ( 0.000000000000000000, 120.0000000000000000, 16.00000000000000000 ) ) ;
#4581=EDGE_CURVE ( 'NONE', #5659, #3152, #6268, .T. ) ;
#4583=CARTESIAN_POINT ( 'NONE',  ( -8.000000000000007105, 72.93807001241029297, 12.00000000000000000 ) ) ;
#4585=VECTOR ( 'NONE', #3404, 1000.000000000000000 ) ;
#4591=DIRECTION ( 'NONE',  ( -0.000000000000000000, -0.000000000000000000, -1.000000000000000000 ) ) ;
#4600=CIRCLE ( 'NONE', #188, 21.00000000000000355 ) ;
#4605=CARTESIAN_POINT ( 'NONE',  ( 174.7835321302054865, 68.75545066608756883, 1.999999999999994893 ) ) ;
#4607=VECTOR ( 'NONE', #3106, 1000.000000000000000 ) ;
#4614=ORIENTED_EDGE ( 'NONE', *, *, #5795, .F. ) ;
#4616=AXIS2_PLACEMENT_3D ( 'NONE', #3499, #4917, #4004 ) ;
#4629=VERTEX_POINT ( 'NONE', #2760 ) ;
#4633=DIRECTION ( 'NONE',  ( 1.000000000000000000, 0.000000000000000000, 0.000000000000000000 ) ) ;
#4639=DIRECTION ( 'NONE',  ( -1.000000000000000000, 0.000000000000000000, 0.000000000000000000 ) ) ;
#4644=ORIENTED_EDGE ( 'NONE', *, *, #700, .T. ) ;
#4649=DIRECTION ( 'NONE',  ( -0.000000000000000000, -0.000000000000000000, -1.000000000000000000 ) ) ;
#4650=DIRECTION ( 'NONE',  ( -0.000000000000000000, -0.000000000000000000, -1.000000000000000000 ) ) ;
#4655=ORIENTED_EDGE ( 'NONE', *, *, #2973, .F. ) ;
#4662=DIRECTION ( 'NONE',  ( -1.000000000000000000, 0.000000000000000000, 0.000000000000000000 ) ) ;
#4663=FACE_OUTER_BOUND ( 'NONE', #512, .T. ) ;
#4683=CIRCLE ( 'NONE', #263, 166.8359700257217071 ) ;
#4684=ORIENTED_EDGE ( 'NONE', *, *, #3017, .T. ) ;
#4685=DIRECTION ( 'NONE',  ( -1.000000000000000000, -1.852483853906148286E-16, 0.000000000000000000 ) ) ;
#4691=CARTESIAN_POINT ( 'NONE',  ( 19.25293315802950644, 8.385974291186926166, 12.00000000000000000 ) ) ;
#4696=PRODUCT_DEFINITION_CONTEXT ( 'detailed design', #3361, 'design' ) ;
#4697=CARTESIAN_POINT ( 'NONE',  ( 0.000000000000000000, 120.0000000000000000, 12.00000000000000000 ) ) ;
#4698=CARTESIAN_POINT ( 'NONE',  ( -8.000000000000021316, 1.729804722550182166E-15, 9.999999999999987566 ) ) ;
#4703=VERTEX_POINT ( 'NONE', #1483 ) ;
#4726=AXIS2_PLACEMENT_3D ( 'NONE', #4230, #1430, #888 ) ;
#4727=VECTOR ( 'NONE', #1763, 1000.000000000000000 ) ;
#4734=AXIS2_PLACEMENT_3D ( 'NONE', #4133, #1568, #3177 ) ;
#4742=AXIS2_PLACEMENT_3D ( 'NONE', #557, #2922, #4899 ) ;
#4743=AXIS2_PLACEMENT_3D ( 'NONE', #4331, #2842, #4818 ) ;
#4748=DIRECTION ( 'NONE',  ( -0.000000000000000000, -0.000000000000000000, -1.000000000000000000 ) ) ;
#4750=LINE ( 'NONE', #3298, #5249 ) ;
#4753=ADVANCED_FACE ( 'NONE', ( #6344 ), #2996, .F. ) ;
#4758=EDGE_CURVE ( 'NONE', #823, #81, #2960, .T. ) ;
#4779=ADVANCED_FACE ( 'NONE', ( #4375, #1935 ), #2028, .F. ) ;
#4780=DIRECTION ( 'NONE',  ( -1.000000000000000000, 0.000000000000000000, 0.000000000000000000 ) ) ;
#4785=CARTESIAN_POINT ( 'NONE',  ( -6.500000000000000000, 134.5953136438507158, 12.00000000000000000 ) ) ;
#4790=AXIS2_PLACEMENT_3D ( 'NONE', #1938, #3896, #1999 ) ;
#4792=DIRECTION ( 'NONE',  ( 1.000000000000000000, 3.576835832488757469E-15, 0.000000000000000000 ) ) ;
#4794=CARTESIAN_POINT ( 'NONE',  ( 17.05141243254541550, -24.25762350764758679, 0.000000000000000000 ) ) ;
#4795=PLANE ( 'NONE',  #3661 ) ;
#4796=DIRECTION ( 'NONE',  ( 1.000000000000000000, 0.000000000000000000, 0.000000000000000000 ) ) ;
#4802=DIRECTION ( 'NONE',  ( 0.000000000000000000, 0.000000000000000000, 1.000000000000000000 ) ) ;
#4807=ORIENTED_EDGE ( 'NONE', *, *, #699, .F. ) ;
#4810=VECTOR ( 'NONE', #3034, 1000.000000000000000 ) ;
#4814=AXIS2_PLACEMENT_3D ( 'NONE', #1515, #948, #4472 ) ;
#4816=ORIENTED_EDGE ( 'NONE', *, *, #2973, .T. ) ;
#4818=DIRECTION ( 'NONE',  ( 1.000000000000000000, 0.000000000000000000, 0.000000000000000000 ) ) ;
#4821=ORIENTED_EDGE ( 'NONE', *, *, #607, .F. ) ;
#4827=VECTOR ( 'NONE', #5590, 1000.000000000000000 ) ;
#4829=DIRECTION ( 'NONE',  ( -0.000000000000000000, -0.000000000000000000, -1.000000000000000000 ) ) ;
#4837=EDGE_CURVE ( 'NONE', #4, #2027, #6277, .T. ) ;
#4856=DIRECTION ( 'NONE',  ( 1.000000000000000000, 0.000000000000000000, 0.000000000000000000 ) ) ;
#4859=EDGE_CURVE ( 'NONE', #4017, #341, #612, .T. ) ;
#4860=DIRECTION ( 'NONE',  ( -2.295390878742131754E-32, 1.239088197126290570E-16, -1.000000000000000000 ) ) ;
#4862=ORIENTED_EDGE ( 'NONE', *, *, #3017, .F. ) ;
#4869=ORIENTED_EDGE ( 'NONE', *, *, #1789, .T. ) ;
#4875=DIRECTION ( 'NONE',  ( -1.000000000000000000, -1.852483853906148286E-16, 0.000000000000000000 ) ) ;
#4877=LINE ( 'NONE', #5336, #2761 ) ;
#4880=ORIENTED_EDGE ( 'NONE', *, *, #521, .F. ) ;
#4886=EDGE_CURVE ( 'NONE', #990, #1906, #516, .T. ) ;
#4891=CARTESIAN_POINT ( 'NONE',  ( 6.500000000000001776, 120.0000000000000000, 12.00000000000000000 ) ) ;
#4899=DIRECTION ( 'NONE',  ( 0.000000000000000000, 0.000000000000000000, 1.000000000000000000 ) ) ;
#4905=CARTESIAN_POINT ( 'NONE',  ( 12.72356008887154211, 29.12127642700182051, 9.800582165931864154 ) ) ;
#4909=DIRECTION ( 'NONE',  ( 0.000000000000000000, 0.000000000000000000, 1.000000000000000000 ) ) ;
#4913=VERTEX_POINT ( 'NONE', #5522 ) ;
#4915=ORIENTED_EDGE ( 'NONE', *, *, #473, .T. ) ;
#4917=DIRECTION ( 'NONE',  ( -0.000000000000000000, 0.000000000000000000, 1.000000000000000000 ) ) ;
#4920=VERTEX_POINT ( 'NONE', #5439 ) ;
#4926=AXIS2_PLACEMENT_3D ( 'NONE', #1519, #4937, #2035 ) ;
#4929=CARTESIAN_POINT ( 'NONE',  ( 21.00000000000000355, 2.571758278209442056E-15, 12.00000000000000000 ) ) ;
#4930=VERTEX_POINT ( 'NONE', #1988 ) ;
#4937=DIRECTION ( 'NONE',  ( -2.295390878742131754E-32, 1.239088197126290570E-16, -1.000000000000000000 ) ) ;
#4945=ORIENTED_EDGE ( 'NONE', *, *, #2656, .F. ) ;
#4950=AXIS2_PLACEMENT_3D ( 'NONE', #4363, #6333, #3639 ) ;
#4952=EDGE_CURVE ( 'NONE', #647, #3460, #4399, .T. ) ;
#4955=EDGE_CURVE ( 'NONE', #1278, #5526, #925, .T. ) ;
#4957=B_SPLINE_CURVE_WITH_KNOTS ( 'NONE', 3,
 ( #3941, #3005, #1520, #4970, #4905, #501, #536, #5946, #2420, #1553, #4423, #4384, #5914, #4994, #1491, #3487, #1010, #5458 ),
 .UNSPECIFIED., .F., .F.,
 ( 4, 2, 2, 2, 2, 2, 2, 2, 4 ),
 ( 0.000000000000000000, 0.0007936035350328099784, 0.001587207070065619957, 0.002380810605098429827, 0.003174414140131239914, 0.003968017675164050434, 0.004761621210196859653, 0.005555224745229667138, 0.006348828280262475490 ),
 .UNSPECIFIED. ) ;
#4966=CARTESIAN_POINT ( 'NONE',  ( -12.72367524380681303, 29.12081030169100870, 2.199628915743095270 ) ) ;
#4967=DIRECTION ( 'NONE',  ( 0.000000000000000000, -1.000000000000000000, -1.239088197126290570E-16 ) ) ;
#4970=CARTESIAN_POINT ( 'NONE',  ( 12.66240722304475064, 29.37208741619408059, 9.875474163642433467 ) ) ;
#4972=FACE_OUTER_BOUND ( 'NONE', #95, .T. ) ;
#4978=ORIENTED_EDGE ( 'NONE', *, *, #1600, .F. ) ;
#4979=DIRECTION ( 'NONE',  ( 0.000000000000000000, 1.000000000000000000, -0.000000000000000000 ) ) ;
#4982=ORIENTED_EDGE ( 'NONE', *, *, #1486, .T. ) ;
#4994=CARTESIAN_POINT ( 'NONE',  ( 13.35972283035915531, 26.60564881331300668, 7.306817940158689240 ) ) ;
#4995=AXIS2_PLACEMENT_3D ( 'NONE', #4565, #4501, #3599 ) ;
#4998=DIRECTION ( 'NONE',  ( 0.000000000000000000, 1.000000000000000000, 1.247733429937938623E-16 ) ) ;
#4999=VERTEX_POINT ( 'NONE', #5988 ) ;
#5001=AXIS2_PLACEMENT_3D ( 'NONE', #5276, #4748, #4780 ) ;
#5002=VECTOR ( 'NONE', #4231, 1000.000000000000000 ) ;
#5004=CARTESIAN_POINT ( 'NONE',  ( -8.000000000000000000, 110.3953136438507130, 12.00000000000000000 ) ) ;
#5005=CARTESIAN_POINT ( 'NONE',  ( 13.15471301119415770, 27.39842886758933105, 3.337628543836456796 ) ) ;
#5006=LINE ( 'NONE', #5494, #6066 ) ;
#5007=CIRCLE ( 'NONE', #3358, 21.00000000000000355 ) ;
#5008=CARTESIAN_POINT ( 'NONE',  ( 8.000000000000007105, 72.93807001241029297, 12.00000000000000000 ) ) ;
#5016=DIRECTION ( 'NONE',  ( 1.000000000000000000, 0.000000000000000000, 0.000000000000000000 ) ) ;
#5025=CYLINDRICAL_SURFACE ( 'NONE', #6281, 166.8359700257217071 ) ;
#5026=EDGE_LOOP ( 'NONE', ( #4498, #5762, #5779, #6082 ) ) ;
#5037=ORIENTED_EDGE ( 'NONE', *, *, #29, .F. ) ;
#5042=CARTESIAN_POINT ( 'NONE',  ( 12.47907056128239667, 30.13454381782201352, 1.999999999999989120 ) ) ;
#5054=AXIS2_PLACEMENT_3D ( 'NONE', #2616, #2104, #1533 ) ;
#5055=ORIENTED_EDGE ( 'NONE', *, *, #4758, .T. ) ;
#5059=EDGE_CURVE ( 'NONE', #1760, #4920, #5006, .T. ) ;
#5072=EDGE_CURVE ( 'NONE', #1184, #341, #2947, .T. ) ;
#5076=CARTESIAN_POINT ( 'NONE',  ( 13.38023260448823848, 26.52727575619375244, 4.947004611186090806 ) ) ;
#5108=CARTESIAN_POINT ( 'NONE',  ( 18.00000000000001421, 26.39531364385072010, 5.999999999999990230 ) ) ;
#5111=AXIS2_PLACEMENT_3D ( 'NONE', #3308, #966, #4792 ) ;
#5114=CARTESIAN_POINT ( 'NONE',  ( 6.500000000000000000, 134.5953136438507158, 12.00000000000000000 ) ) ;
#5117=CARTESIAN_POINT ( 'NONE',  ( -12.50000000000001421, 120.0000000000000000, 16.00000000000000000 ) ) ;
#5120=DIRECTION ( 'NONE',  ( 1.000000000000000000, 0.000000000000000000, 0.000000000000000000 ) ) ;
#5121=DIRECTION ( 'NONE',  ( 0.000000000000000000, 0.000000000000000000, 1.000000000000000000 ) ) ;
#5124=CARTESIAN_POINT ( 'NONE',  ( 6.500000000000000000, 134.5953136438507158, 12.00000000000000000 ) ) ;
#5131=DIRECTION ( 'NONE',  ( -0.000000000000000000, -0.000000000000000000, -1.000000000000000000 ) ) ;
#5135=LINE ( 'NONE', #1196, #479 ) ;
#5145=ORIENTED_EDGE ( 'NONE', *, *, #4064, .T. ) ;
#5146=EDGE_CURVE ( 'NONE', #2807, #4, #3722, .T. ) ;
#5159=CARTESIAN_POINT ( 'NONE',  ( 7.947562104483774093, 68.75545066608756883, 1.999999999999994893 ) ) ;
#5164=DIRECTION ( 'NONE',  ( -0.000000000000000000, 0.000000000000000000, 1.000000000000000000 ) ) ;
#5173=ORIENTED_EDGE ( 'NONE', *, *, #5288, .T. ) ;
#5181=AXIS2_PLACEMENT_3D ( 'NONE', #46, #4322, #2453 ) ;
#5228=VECTOR ( 'NONE', #1555, 1000.000000000000000 ) ;
#5234=ORIENTED_EDGE ( 'NONE', *, *, #5989, .T. ) ;
#5237=EDGE_CURVE ( 'NONE', #1266, #3016, #1621, .T. ) ;
#5239=CARTESIAN_POINT ( 'NONE',  ( 17.05141243254545458, -2.957948544529944430E-14, 12.00000000000000000 ) ) ;
#5241=DIRECTION ( 'NONE',  ( -0.000000000000000000, -0.000000000000000000, -1.000000000000000000 ) ) ;
#5243=ORIENTED_EDGE ( 'NONE', *, *, #786, .F. ) ;
#5249=VECTOR ( 'NONE', #1857, 1000.000000000000000 ) ;
#5253=VECTOR ( 'NONE', #2128, 1000.000000000000000 ) ;
#5264=CLOSED_SHELL ( 'NONE', ( #4192, #114, #3882, #3685, #2729, #1878, #2872, #1331, #1829, #3443, #506, #3330, #2943, #1357, #4104, #6064, #4009, #267, #1322, #2193, #3691, #5430, #76, #2585, #3742, #5700, #3255, #1127, #4779, #940, #1891, #1638, #4753, #6230, #3403 ) ) ;
#5268=( GEOMETRIC_REPRESENTATION_CONTEXT ( 3 ) GLOBAL_UNCERTAINTY_ASSIGNED_CONTEXT ( ( #1212 ) ) GLOBAL_UNIT_ASSIGNED_CONTEXT ( ( #3670, #173, #4081 ) ) REPRESENTATION_CONTEXT ( 'NONE', 'WORKASPACE' ) );
#5275=AXIS2_PLACEMENT_3D ( 'NONE', #4566, #5121, #2665 ) ;
#5276=CARTESIAN_POINT ( 'NONE',  ( 0.000000000000000000, 0.000000000000000000, 12.00000000000000000 ) ) ;
#5282=ORIENTED_EDGE ( 'NONE', *, *, #5456, .F. ) ;
#5286=VERTEX_POINT ( 'NONE', #2365 ) ;
#5287=CARTESIAN_POINT ( 'NONE',  ( 16.00000000000000000, 1.959434878635765131E-15, 12.00000000000000000 ) ) ;
#5288=EDGE_CURVE ( 'NONE', #4913, #5734, #5870, .T. ) ;
#5294=DIRECTION ( 'NONE',  ( -1.852483853906148040E-16, 1.000000000000000000, 1.239088197126290570E-16 ) ) ;
#5307=ORIENTED_EDGE ( 'NONE', *, *, #6304, .F. ) ;
#5309=CARTESIAN_POINT ( 'NONE',  ( -13.35972283035916774, 26.60564881331300668, 7.306817940158690128 ) ) ;
#5313=CIRCLE ( 'NONE', #4995, 16.00000000000000355 ) ;
#5314=CARTESIAN_POINT ( 'NONE',  ( 8.000000000000021316, 1.729804722550182166E-15, 9.999999999999987566 ) ) ;
#5321=ORIENTED_EDGE ( 'NONE', *, *, #2934, .T. ) ;
#5331=ORIENTED_EDGE ( 'NONE', *, *, #4952, .T. ) ;
#5336=CARTESIAN_POINT ( 'NONE',  ( -12.50000000000000355, 120.0000000000000000, 12.00000000000000000 ) ) ;
#5344=CARTESIAN_POINT ( 'NONE',  ( -12.72356008887154033, 29.12127642700181340, 9.800582165931858825 ) ) ;
#5352=CARTESIAN_POINT ( 'NONE',  ( 6.500000000000000000, 0.000000000000000000, 12.00000000000000000 ) ) ;
#5354=CARTESIAN_POINT ( 'NONE',  ( 18.00000000000000355, 100.3953136438507272, 10.00000000000000000 ) ) ;
#5356=FACE_OUTER_BOUND ( 'NONE', #2291, .T. ) ;
#5364=CARTESIAN_POINT ( 'NONE',  ( -13.35991119780008773, 26.60492657425308138, 4.695075907386110359 ) ) ;
#5368=ORIENTED_EDGE ( 'NONE', *, *, #5715, .F. ) ;
#5376=ORIENTED_EDGE ( 'NONE', *, *, #2859, .T. ) ;
#5379=CARTESIAN_POINT ( 'NONE',  ( -13.15428815592194134, 27.40009807703880185, 8.663997969339835237 ) ) ;
#5393=CARTESIAN_POINT ( 'NONE',  ( -13.00793927997763610, 27.97619002235531838, 2.803925835876298400 ) ) ;
#5394=DIRECTION ( 'NONE',  ( 2.295390878742131754E-32, -1.239088197126290570E-16, 1.000000000000000000 ) ) ;
#5396=ORIENTED_EDGE ( 'NONE', *, *, #1486, .F. ) ;
#5397=DIRECTION ( 'NONE',  ( -1.000000000000000000, 0.000000000000000000, 0.000000000000000000 ) ) ;
#5402=ORIENTED_EDGE ( 'NONE', *, *, #6019, .F. ) ;
#5404=ORIENTED_EDGE ( 'NONE', *, *, #3415, .F. ) ;
#5418=AXIS2_PLACEMENT_3D ( 'NONE', #2500, #4460, #1099 ) ;
#5419=CARTESIAN_POINT ( 'NONE',  ( -12.89959272829392667, 28.40844700521620680, 2.518705683379065974 ) ) ;
#5422=ORIENTED_EDGE ( 'NONE', *, *, #679, .F. ) ;
#5425=FACE_OUTER_BOUND ( 'NONE', #1308, .T. ) ;
#5430=ADVANCED_FACE ( 'NONE', ( #3322 ), #5852, .T. ) ;
#5435=ORIENTED_EDGE ( 'NONE', *, *, #5902, .T. ) ;
#5438=CARTESIAN_POINT ( 'NONE',  ( 12.66355262481067889, 29.36736923042837333, 2.125736663006382088 ) ) ;
#5439=CARTESIAN_POINT ( 'NONE',  ( 8.000000000000005329, 110.3953136438506988, 0.000000000000000000 ) ) ;
#5446=PLANE ( 'NONE',  #4533 ) ;
#5448=FACE_BOUND ( 'NONE', #6241, .T. ) ;
#5454=FACE_OUTER_BOUND ( 'NONE', #3509, .T. ) ;
#5456=EDGE_CURVE ( 'NONE', #823, #2013, #4600, .T. ) ;
#5458=CARTESIAN_POINT ( 'NONE',  ( 13.41482486054668399, 26.39531364385071655, 5.999999999999990230 ) ) ;
#5464=ORIENTED_EDGE ( 'NONE', *, *, #1194, .F. ) ;
#5478=DIRECTION ( 'NONE',  ( -1.000000000000000000, -1.852483853906148286E-16, 0.000000000000000000 ) ) ;
#5486=CARTESIAN_POINT ( 'NONE',  ( 17.05141243254545458, -2.957948544529944430E-14, 0.000000000000000000 ) ) ;
#5490=ORIENTED_EDGE ( 'NONE', *, *, #6019, .T. ) ;
#5494=CARTESIAN_POINT ( 'NONE',  ( 8.000000000000000000, 110.3953136438507130, 12.00000000000000000 ) ) ;
#5501=CARTESIAN_POINT ( 'NONE',  ( 8.000000000000021316, 1.481987083124922376E-15, 12.00000000000000000 ) ) ;
#5507=CARTESIAN_POINT ( 'NONE',  ( 0.000000000000000000, 120.0000000000000000, 16.00000000000000000 ) ) ;
#5514=CARTESIAN_POINT ( 'NONE',  ( -8.000000000000000000, 110.3953136438507130, 12.00000000000000000 ) ) ;
#5521=CARTESIAN_POINT ( 'NONE',  ( -16.00000000000000355, 0.000000000000000000, -4.000000000000000000 ) ) ;
#5522=CARTESIAN_POINT ( 'NONE',  ( 6.500000000000005329, 120.0000000000000000, -4.000000000000000000 ) ) ;
#5523=DIRECTION ( 'NONE',  ( 1.000000000000000000, 0.000000000000000000, 0.000000000000000000 ) ) ;
#5526=VERTEX_POINT ( 'NONE', #3008 ) ;
#5527=EDGE_CURVE ( 'NONE', #2807, #1433, #4390, .T. ) ;
#5532=DIRECTION ( 'NONE',  ( -0.000000000000000000, 0.000000000000000000, 1.000000000000000000 ) ) ;
#5548=EDGE_CURVE ( 'NONE', #6319, #1301, #4481, .T. ) ;
#5561=CARTESIAN_POINT ( 'NONE',  ( 7.947562104483774093, 68.75545066608756883, 12.00000000000000000 ) ) ;
#5565=ORIENTED_EDGE ( 'NONE', *, *, #2197, .T. ) ;
#5572=EDGE_LOOP ( 'NONE', ( #1726, #3867, #2176, #5980 ) ) ;
#5590=DIRECTION ( 'NONE',  ( -0.000000000000000000, -0.000000000000000000, -1.000000000000000000 ) ) ;
#5592=CARTESIAN_POINT ( 'NONE',  ( 12.50000000000001421, 120.0000000000000000, 16.00000000000000000 ) ) ;
#5593=EDGE_LOOP ( 'NONE', ( #5402, #1175, #380, #3119, #3011, #4655, #4457 ) ) ;
#5603=CARTESIAN_POINT ( 'NONE',  ( 18.00000000000000355, 100.3953136438507272, 10.00000000000000000 ) ) ;
#5611=EDGE_LOOP ( 'NONE', ( #2165, #2959, #2994, #5891 ) ) ;
#5615=AXIS2_PLACEMENT_3D ( 'NONE', #646, #1566, #675 ) ;
#5617=FACE_OUTER_BOUND ( 'NONE', #848, .T. ) ;
#5625=EDGE_CURVE ( 'NONE', #2831, #1433, #4147, .T. ) ;
#5628=AXIS2_PLACEMENT_3D ( 'NONE', #5998, #4043, #3057 ) ;
#5638=CYLINDRICAL_SURFACE ( 'NONE', #129, 12.50000000000000355 ) ;
#5644=CARTESIAN_POINT ( 'NONE',  ( 0.000000000000000000, 0.000000000000000000, 12.00000000000000000 ) ) ;
#5658=DIRECTION ( 'NONE',  ( -1.000000000000000000, 0.000000000000000000, 0.000000000000000000 ) ) ;
#5659=VERTEX_POINT ( 'NONE', #2804 ) ;
#5679=FACE_BOUND ( 'NONE', #4244, .T. ) ;
#5684=LINE ( 'NONE', #6132, #276 ) ;
#5690=AXIS2_PLACEMENT_3D ( 'NONE', #1011, #1390, #3351 ) ;
#5691=CARTESIAN_POINT ( 'NONE',  ( 0.000000000000000000, -24.25762350764758679, 12.00000000000000000 ) ) ;
#5694=ORIENTED_EDGE ( 'NONE', *, *, #3898, .F. ) ;
#5700=ADVANCED_FACE ( 'NONE', ( #5679, #2288 ), #5712, .F. ) ;
#5712=PLANE ( 'NONE',  #83 ) ;
#5715=EDGE_CURVE ( 'NONE', #1906, #2036, #3346, .T. ) ;
#5722=DIRECTION ( 'NONE',  ( 1.000000000000000000, 0.000000000000000000, 0.000000000000000000 ) ) ;
#5730=CARTESIAN_POINT ( 'NONE',  ( -12.89883946988004304, 28.41146683342871171, 9.483046795230265502 ) ) ;
#5734=VERTEX_POINT ( 'NONE', #3749 ) ;
#5758=CARTESIAN_POINT ( 'NONE',  ( -17.05141243254543681, -12.25762350764760455, 12.00000000000000000 ) ) ;
#5762=ORIENTED_EDGE ( 'NONE', *, *, #5237, .T. ) ;
#5765=VECTOR ( 'NONE', #527, 1000.000000000000000 ) ;
#5774=SHAPE_REPRESENTATION_RELATIONSHIP ( 'NONE' , 'NONE' ,  #3711, #4474 ) ;
#5779=ORIENTED_EDGE ( 'NONE', *, *, #786, .T. ) ;
#5781=AXIS2_PLACEMENT_3D ( 'NONE', #4605, #3547, #724 ) ;
#5790=LINE ( 'NONE', #6266, #2219 ) ;
#5794=VERTEX_POINT ( 'NONE', #4447 ) ;
#5795=EDGE_CURVE ( 'NONE', #341, #5286, #3279, .T. ) ;
#5796=EDGE_LOOP ( 'NONE', ( #4945, #6049, #5321, #5396 ) ) ;
#5798=CARTESIAN_POINT ( 'NONE',  ( -13.05961095629095503, 27.77190499716703442, 9.030829679283291611 ) ) ;
#5802=( NAMED_UNIT ( * ) SI_UNIT ( $, .STERADIAN. ) SOLID_ANGLE_UNIT ( ) );
#5819=FACE_OUTER_BOUND ( 'NONE', #5026, .T. ) ;
#5822=EDGE_LOOP ( 'NONE', ( #1002, #1141, #4029, #3447 ) ) ;
#5823=CARTESIAN_POINT ( 'NONE',  ( 17.05141243254545458, -2.957948544529944430E-14, 12.00000000000000000 ) ) ;
#5824=CARTESIAN_POINT ( 'NONE',  ( -13.40794989232620615, 26.42147665086397268, 6.529465147186705565 ) ) ;
#5827=CIRCLE ( 'NONE', #3038, 166.8359700257217071 ) ;
#5834=DIRECTION ( 'NONE',  ( 0.000000000000000000, -1.000000000000000000, -1.247733429937938623E-16 ) ) ;
#5842=LINE ( 'NONE', #1383, #328 ) ;
#5846=VERTEX_POINT ( 'NONE', #533 ) ;
#5848=CARTESIAN_POINT ( 'NONE',  ( -0.000000000000000000, 134.5953136438507158, 0.000000000000000000 ) ) ;
#5852=PLANE ( 'NONE',  #1309 ) ;
#5862=CARTESIAN_POINT ( 'NONE',  ( -13.41482486054668044, 26.39531364385071299, 5.999999999999990230 ) ) ;
#5870=CIRCLE ( 'NONE', #4726, 6.500000000000005329 ) ;
#5872=LINE ( 'NONE', #4891, #6043 ) ;
#5873=CARTESIAN_POINT ( 'NONE',  ( 0.000000000000000000, -24.25762350764758679, 12.00000000000000000 ) ) ;
#5883=PLANE ( 'NONE',  #5690 ) ;
#5884=AXIS2_PLACEMENT_3D ( 'NONE', #5644, #655, #4639 ) ;
#5890=ORIENTED_EDGE ( 'NONE', *, *, #104, .T. ) ;
#5891=ORIENTED_EDGE ( 'NONE', *, *, #4581, .T. ) ;
#5893=APPLICATION_CONTEXT ( 'automotive_design' ) ;
#5896=VERTEX_POINT ( 'NONE', #5940 ) ;
#5902=EDGE_CURVE ( 'NONE', #5846, #3758, #3872, .T. ) ;
#5905=CARTESIAN_POINT ( 'NONE',  ( -6.500000000000006217, 130.6770782520313219, 0.000000000000000000 ) ) ;
#5910=CARTESIAN_POINT ( 'NONE',  ( -12.66355262481067179, 29.36736923042837333, 2.125736663006382976 ) ) ;
#5911=LINE ( 'NONE', #1517, #2152 ) ;
#5912=VERTEX_POINT ( 'NONE', #3150 ) ;
#5914=CARTESIAN_POINT ( 'NONE',  ( 13.30659111572998654, 26.80965796039522786, 7.792318603440350877 ) ) ;
#5915=CYLINDRICAL_SURFACE ( 'NONE', #2395, 166.8359700257217071 ) ;
#5919=ORIENTED_EDGE ( 'NONE', *, *, #2734, .F. ) ;
#5922=ORIENTED_EDGE ( 'NONE', *, *, #1342, .F. ) ;
#5940=CARTESIAN_POINT ( 'NONE',  ( 8.000000000000003553, 100.3953136438507272, 10.00000000000000000 ) ) ;
#5946=CARTESIAN_POINT ( 'NONE',  ( 13.00740645622773961, 27.97830129128179166, 9.197704556789860320 ) ) ;
#5950=CARTESIAN_POINT ( 'NONE',  ( -8.000000000000003553, 100.3953136438507272, 10.00000000000000000 ) ) ;
#5963=DIRECTION ( 'NONE',  ( -1.000000000000000000, 0.000000000000000000, 0.000000000000000000 ) ) ;
#5965=CARTESIAN_POINT ( 'NONE',  ( 0.000000000000000000, 0.000000000000000000, -4.000000000000000000 ) ) ;
#5978=CARTESIAN_POINT ( 'NONE',  ( -174.7835321302054865, 68.75545066608756883, 9.999999999999996447 ) ) ;
#5980=ORIENTED_EDGE ( 'NONE', *, *, #5715, .T. ) ;
#5983=CARTESIAN_POINT ( 'NONE',  ( 0.000000000000000000, 0.000000000000000000, -4.000000000000000000 ) ) ;
#5987=CARTESIAN_POINT ( 'NONE',  ( 12.54137761259614514, 29.87368101119752950, 2.025772336917471161 ) ) ;
#5988=CARTESIAN_POINT ( 'NONE',  ( -16.00000000000000355, 0.000000000000000000, 16.00000000000000000 ) ) ;
#5989=EDGE_CURVE ( 'NONE', #862, #2130, #1204, .T. ) ;
#5990=EDGE_CURVE ( 'NONE', #4120, #3745, #3353, .T. ) ;
#5996=ORIENTED_EDGE ( 'NONE', *, *, #5456, .T. ) ;
#5998=CARTESIAN_POINT ( 'NONE',  ( 0.000000000000000000, 0.000000000000000000, -4.000000000000000000 ) ) ;
#6008=ORIENTED_EDGE ( 'NONE', *, *, #2508, .T. ) ;
#6009=ORIENTED_EDGE ( 'NONE', *, *, #4400, .F. ) ;
#6013=CARTESIAN_POINT ( 'NONE',  ( 13.41482486054668399, 26.39531364385071655, 5.999999999999990230 ) ) ;
#6016=CARTESIAN_POINT ( 'NONE',  ( 0.000000000000000000, 0.000000000000000000, 0.000000000000000000 ) ) ;
#6019=EDGE_CURVE ( 'NONE', #5896, #3054, #3632, .T. ) ;
#6023=EDGE_CURVE ( 'NONE', #81, #434, #908, .T. ) ;
#6028=CIRCLE ( 'NONE', #3861, 21.00000000000000355 ) ;
#6030=EDGE_LOOP ( 'NONE', ( #4097, #2122, #1257, #3325, #1104, #63, #2003 ) ) ;
#6033=DIRECTION ( 'NONE',  ( -1.000000000000000000, 0.000000000000000000, 0.000000000000000000 ) ) ;
#6036=CARTESIAN_POINT ( 'NONE',  ( 18.00000000000000355, 100.3953136438507272, 1.999999999999998224 ) ) ;
#6041=ORIENTED_EDGE ( 'NONE', *, *, #6179, .F. ) ;
#6043=VECTOR ( 'NONE', #4829, 1000.000000000000000 ) ;
#6049=ORIENTED_EDGE ( 'NONE', *, *, #6179, .T. ) ;
#6056=VECTOR ( 'NONE', #3923, 1000.000000000000000 ) ;
#6064=ADVANCED_FACE ( 'NONE', ( #2694 ), #4795, .F. ) ;
#6066=VECTOR ( 'NONE', #1075, 1000.000000000000000 ) ;
#6067=PRODUCT ( 'Part 32,5_Varsay\X2\0131\X0\lan', 'Part 32,5_Varsay\X2\0131\X0\lan', '', ( #159 ) ) ;
#6076=DIRECTION ( 'NONE',  ( -1.000000000000000000, -1.852483853906148286E-16, 0.000000000000000000 ) ) ;
#6081=CARTESIAN_POINT ( 'NONE',  ( 12.50000000000001421, 120.0000000000000000, -4.000000000000000000 ) ) ;
#6082=ORIENTED_EDGE ( 'NONE', *, *, #1247, .F. ) ;
#6095=CYLINDRICAL_SURFACE ( 'NONE', #5884, 16.00000000000000000 ) ;
#6100=ORIENTED_EDGE ( 'NONE', *, *, #104, .F. ) ;
#6109=ORIENTED_EDGE ( 'NONE', *, *, #2547, .F. ) ;
#6120=DIRECTION ( 'NONE',  ( 1.000000000000000000, 0.000000000000000000, 0.000000000000000000 ) ) ;
#6121=DIRECTION ( 'NONE',  ( -1.000000000000000000, 0.000000000000000000, 0.000000000000000000 ) ) ;
#6129=CIRCLE ( 'NONE', #166, 6.500000000000005329 ) ;
#6132=CARTESIAN_POINT ( 'NONE',  ( 6.500000000000000000, 0.000000000000000000, 0.000000000000000000 ) ) ;
#6135=VECTOR ( 'NONE', #4979, 1000.000000000000000 ) ;
#6138=CARTESIAN_POINT ( 'NONE',  ( 18.00000000000001421, 30.39531364385072010, 1.999999999999989564 ) ) ;
#6152=ORIENTED_EDGE ( 'NONE', *, *, #5990, .T. ) ;
#6154=ORIENTED_EDGE ( 'NONE', *, *, #5059, .T. ) ;
#6165=CIRCLE ( 'NONE', #3382, 12.50000000000001421 ) ;
#6168=CARTESIAN_POINT ( 'NONE',  ( 174.7835321302054865, 68.75545066608756883, 0.000000000000000000 ) ) ;
#6172=AXIS2_PLACEMENT_3D ( 'NONE', #4380, #11, #3446 ) ;
#6173=ORIENTED_EDGE ( 'NONE', *, *, #5527, .F. ) ;
#6177=EDGE_CURVE ( 'NONE', #3054, #2143, #2345, .T. ) ;
#6179=EDGE_CURVE ( 'NONE', #990, #1518, #896, .T. ) ;
#6182=ORIENTED_EDGE ( 'NONE', *, *, #28, .F. ) ;
#6188=DIRECTION ( 'NONE',  ( -0.000000000000000000, 0.000000000000000000, 1.000000000000000000 ) ) ;
#6200=VERTEX_POINT ( 'NONE', #1352 ) ;
#6223=EDGE_CURVE ( 'NONE', #5286, #2807, #1512, .T. ) ;
#6230=ADVANCED_FACE ( 'NONE', ( #1102 ), #1965, .T. ) ;
#6233=ORIENTED_EDGE ( 'NONE', *, *, #5072, .F. ) ;
#6238=FACE_OUTER_BOUND ( 'NONE', #1095, .T. ) ;
#6241=EDGE_LOOP ( 'NONE', ( #1663, #1255, #212, #3565 ) ) ;
#6243=VECTOR ( 'NONE', #1682, 1000.000000000000000 ) ;
#6245=CARTESIAN_POINT ( 'NONE',  ( -13.30659111572999720, 26.80965796039522431, 7.792318603440349989 ) ) ;
#6246=DIRECTION ( 'NONE',  ( 0.000000000000000000, -0.000000000000000000, 1.000000000000000000 ) ) ;
#6263=VECTOR ( 'NONE', #4196, 1000.000000000000000 ) ;
#6266=CARTESIAN_POINT ( 'NONE',  ( 18.00000000000001421, 30.39531364385072010, 9.999999999999991118 ) ) ;
#6268=CIRCLE ( 'NONE', #3689, 12.50000000000001421 ) ;
#6277=LINE ( 'NONE', #3792, #1108 ) ;
#6281=AXIS2_PLACEMENT_3D ( 'NONE', #257, #1642, #6121 ) ;
#6284=CARTESIAN_POINT ( 'NONE',  ( 0.000000000000000000, 0.000000000000000000, 12.00000000000000000 ) ) ;
#6291=EDGE_CURVE ( 'NONE', #1805, #3965, #4491, .T. ) ;
#6293=DIRECTION ( 'NONE',  ( -0.000000000000000000, -0.000000000000000000, -1.000000000000000000 ) ) ;
#6295=ORIENTED_EDGE ( 'NONE', *, *, #29, .T. ) ;
#6297=ORIENTED_EDGE ( 'NONE', *, *, #5146, .T. ) ;
#6304=EDGE_CURVE ( 'NONE', #1433, #3054, #1710, .T. ) ;
#6307=EDGE_CURVE ( 'NONE', #5846, #4913, #5872, .T. ) ;
#6308=DIRECTION ( 'NONE',  ( 0.000000000000000000, 0.000000000000000000, 1.000000000000000000 ) ) ;
#6319=VERTEX_POINT ( 'NONE', #1448 ) ;
#6326=ORIENTED_EDGE ( 'NONE', *, *, #3245, .F. ) ;
#6331=EDGE_LOOP ( 'NONE', ( #1529, #1874, #3848, #5145 ) ) ;
#6332=ORIENTED_EDGE ( 'NONE', *, *, #4270, .F. ) ;
#6333=DIRECTION ( 'NONE',  ( -1.000000000000000000, -1.852483853906148040E-16, 0.000000000000000000 ) ) ;
#6335=CIRCLE ( 'NONE', #4054, 16.00000000000000355 ) ;
#6344=FACE_OUTER_BOUND ( 'NONE', #2703, .T. ) ;
#6349=AXIS2_PLACEMENT_3D ( 'NONE', #290, #2242, #4169 ) ;
#6357=CARTESIAN_POINT ( 'NONE',  ( 0.000000000000000000, 0.000000000000000000, 16.00000000000000000 ) ) ;
#6385=COLOUR_RGB('Light Blue',0.38,0.62,0.78);
#6386=FILL_AREA_STYLE_COLOUR('',#6385);
#6387=FILL_AREA_STYLE('',(#6386));
#6388=SURFACE_STYLE_FILL_AREA(#6387);
#6389=SURFACE_SIDE_STYLE('',(#6388));
#6390=SURFACE_STYLE_USAGE(.BOTH.,#6389);
#6391=PRESENTATION_STYLE_ASSIGNMENT((#6390));
ENDSEC;
END-ISO-10303-21;
